ISO-10303-21;
HEADER;
/* Generated by software containing ST-Developer
 * from STEP Tools, Inc. (www.steptools.com) 
 */

FILE_DESCRIPTION(
/* description */ (''),
/* implementation_level */ '2;1');

FILE_NAME(
/* name */ '08_Piston_Ring_Compressor_D16.step',
/* time_stamp */ '2026-10-25T01:10:36-07:00',
/* author */ (''),
/* organization */ (''),
/* preprocessor_version */ 'ST-DEVELOPER v20.2',
/* originating_system */ 'Autodesk Translation Framework v15.15.0.0',
/* authorisation */ '');

FILE_SCHEMA (('AUTOMOTIVE_DESIGN { 1 0 10303 214 3 1 1 }'));
ENDSEC;

DATA;
#10=MECHANICAL_DESIGN_GEOMETRIC_PRESENTATION_REPRESENTATION('',(#1300),#60365);
#72=SHAPE_REPRESENTATION_RELATIONSHIP('SRR','None',#60412,#82);
#82=ADVANCED_BREP_SHAPE_REPRESENTATION('',(#92),#60360);
#92=MANIFOLD_SOLID_BREP('Body1',#18302);
#127=B_SPLINE_SURFACE_WITH_KNOTS('',3,3,((#45073,#45074,#45075,#45076,#45077,
#45078,#45079,#45080,#45081,#45082,#45083,#45084,#45085,#45086),(#45087,
#45088,#45089,#45090,#45091,#45092,#45093,#45094,#45095,#45096,#45097,#45098,
#45099,#45100),(#45101,#45102,#45103,#45104,#45105,#45106,#45107,#45108,
#45109,#45110,#45111,#45112,#45113,#45114),(#45115,#45116,#45117,#45118,
#45119,#45120,#45121,#45122,#45123,#45124,#45125,#45126,#45127,#45128)),
 .UNSPECIFIED.,.F.,.F.,.F.,(4,4),(4,1,1,1,1,1,1,1,1,1,1,4),(0.,1.),(-3.29679099043599E-16,
0.0888888888888885,0.177777777777777,0.266666666666666,0.275,0.389814814814814,
0.504629629629628,0.619444444444443,0.744444444444442,0.829629629629628,
0.914814814814814,1.),.UNSPECIFIED.);
#128=B_SPLINE_SURFACE_WITH_KNOTS('',3,3,((#45942,#45943,#45944,#45945,#45946,
#45947,#45948,#45949,#45950,#45951,#45952,#45953,#45954,#45955),(#45956,
#45957,#45958,#45959,#45960,#45961,#45962,#45963,#45964,#45965,#45966,#45967,
#45968,#45969),(#45970,#45971,#45972,#45973,#45974,#45975,#45976,#45977,
#45978,#45979,#45980,#45981,#45982,#45983),(#45984,#45985,#45986,#45987,
#45988,#45989,#45990,#45991,#45992,#45993,#45994,#45995,#45996,#45997)),
 .UNSPECIFIED.,.F.,.F.,.F.,(4,4),(4,1,1,1,1,1,1,1,1,1,1,4),(0.,1.),(-4.77815499535063E-15,
0.0888888888888856,0.177777777777776,0.266666666666666,0.275,0.389814814814814,
0.504629629629628,0.619444444444443,0.744444444444442,0.829629584919082,
0.914814725393722,0.999999865868361),.UNSPECIFIED.);
#129=B_SPLINE_SURFACE_WITH_KNOTS('',3,3,((#46017,#46018,#46019,#46020,#46021,
#46022,#46023,#46024,#46025,#46026,#46027,#46028,#46029,#46030,#46031,#46032,
#46033,#46034,#46035,#46036,#46037,#46038,#46039,#46040,#46041,#46042),
(#46043,#46044,#46045,#46046,#46047,#46048,#46049,#46050,#46051,#46052,
#46053,#46054,#46055,#46056,#46057,#46058,#46059,#46060,#46061,#46062,#46063,
#46064,#46065,#46066,#46067,#46068),(#46069,#46070,#46071,#46072,#46073,
#46074,#46075,#46076,#46077,#46078,#46079,#46080,#46081,#46082,#46083,#46084,
#46085,#46086,#46087,#46088,#46089,#46090,#46091,#46092,#46093,#46094),
(#46095,#46096,#46097,#46098,#46099,#46100,#46101,#46102,#46103,#46104,
#46105,#46106,#46107,#46108,#46109,#46110,#46111,#46112,#46113,#46114,#46115,
#46116,#46117,#46118,#46119,#46120)),.UNSPECIFIED.,.F.,.F.,.F.,(4,4),(4,
1,1,1,1,1,1,1,1,1,1,1,1,1,1,1,1,1,1,1,1,1,1,4),(0.,1.),(-1.52611180263545E-7,
0.00277777777777778,0.05,0.102777777777778,0.105555555555556,0.130555555555556,
0.147222222222222,0.15,0.158333333333333,0.218055555555555,0.277777777777777,
0.36111111111111,0.433333333333332,0.466666666666666,0.547222222222221,
0.644444444444443,0.658333333333332,0.686111111111109,0.688888888888887,
0.744444444444442,0.856944444444442,0.969444444444442,0.988888888888886,
1.),.UNSPECIFIED.);
#130=B_SPLINE_SURFACE_WITH_KNOTS('',3,3,((#46935,#46936,#46937,#46938,#46939,
#46940,#46941,#46942,#46943,#46944,#46945,#46946,#46947,#46948,#46949,#46950,
#46951,#46952,#46953,#46954,#46955,#46956,#46957,#46958),(#46959,#46960,
#46961,#46962,#46963,#46964,#46965,#46966,#46967,#46968,#46969,#46970,#46971,
#46972,#46973,#46974,#46975,#46976,#46977,#46978,#46979,#46980,#46981,#46982),
(#46983,#46984,#46985,#46986,#46987,#46988,#46989,#46990,#46991,#46992,
#46993,#46994,#46995,#46996,#46997,#46998,#46999,#47000,#47001,#47002,#47003,
#47004,#47005,#47006),(#47007,#47008,#47009,#47010,#47011,#47012,#47013,
#47014,#47015,#47016,#47017,#47018,#47019,#47020,#47021,#47022,#47023,#47024,
#47025,#47026,#47027,#47028,#47029,#47030)),.UNSPECIFIED.,.F.,.F.,.F.,(4,
4),(4,1,1,1,1,1,1,1,1,1,1,1,1,1,1,1,1,1,1,1,1,4),(0.,1.),(-1.52611180304074E-7,
0.05,0.0527777777777778,0.105555555555556,0.147222222222222,0.15,0.158333333333333,
0.218055555555555,0.277777777777777,0.36111111111111,0.433333333333332,
0.466666666666666,0.547222222222221,0.644444444444443,0.658333333333332,
0.686111111111109,0.688888888888887,0.744444444444442,0.856944444444442,
0.969444444444442,0.988888888888886,1.),.UNSPECIFIED.);
#604=PLANE('',#19227);
#605=PLANE('',#19228);
#606=PLANE('',#19229);
#607=PLANE('',#19230);
#1080=(
BOUNDED_SURFACE()
B_SPLINE_SURFACE(5,1,((#45196,#45197),(#45198,#45199),(#45200,#45201),(#45202,
#45203),(#45204,#45205),(#45206,#45207),(#45208,#45209),(#45210,#45211),
(#45212,#45213),(#45214,#45215),(#45216,#45217),(#45218,#45219),(#45220,
#45221),(#45222,#45223),(#45224,#45225),(#45226,#45227),(#45228,#45229),
(#45230,#45231),(#45232,#45233),(#45234,#45235),(#45236,#45237),(#45238,
#45239),(#45240,#45241),(#45242,#45243),(#45244,#45245),(#45246,#45247),
(#45248,#45249),(#45250,#45251),(#45252,#45253),(#45254,#45255),(#45256,
#45257),(#45258,#45259),(#45260,#45261),(#45262,#45263),(#45264,#45265),
(#45266,#45267),(#45268,#45269),(#45270,#45271),(#45272,#45273),(#45274,
#45275),(#45276,#45277),(#45278,#45279),(#45280,#45281),(#45282,#45283),
(#45284,#45285),(#45286,#45287),(#45288,#45289),(#45290,#45291),(#45292,
#45293),(#45294,#45295),(#45296,#45297),(#45298,#45299),(#45300,#45301),
(#45302,#45303),(#45304,#45305),(#45306,#45307),(#45308,#45309),(#45310,
#45311),(#45312,#45313),(#45314,#45315),(#45316,#45317),(#45318,#45319),
(#45320,#45321),(#45322,#45323),(#45324,#45325),(#45326,#45327),(#45328,
#45329),(#45330,#45331),(#45332,#45333),(#45334,#45335),(#45336,#45337),
(#45338,#45339),(#45340,#45341),(#45342,#45343),(#45344,#45345),(#45346,
#45347),(#45348,#45349),(#45350,#45351),(#45352,#45353),(#45354,#45355),
(#45356,#45357),(#45358,#45359),(#45360,#45361),(#45362,#45363),(#45364,
#45365),(#45366,#45367),(#45368,#45369),(#45370,#45371),(#45372,#45373),
(#45374,#45375),(#45376,#45377),(#45378,#45379),(#45380,#45381),(#45382,
#45383),(#45384,#45385),(#45386,#45387),(#45388,#45389),(#45390,#45391),
(#45392,#45393),(#45394,#45395),(#45396,#45397),(#45398,#45399),(#45400,
#45401),(#45402,#45403),(#45404,#45405),(#45406,#45407),(#45408,#45409),
(#45410,#45411),(#45412,#45413),(#45414,#45415),(#45416,#45417),(#45418,
#45419),(#45420,#45421),(#45422,#45423),(#45424,#45425),(#45426,#45427),
(#45428,#45429),(#45430,#45431),(#45432,#45433),(#45434,#45435),(#45436,
#45437),(#45438,#45439),(#45440,#45441),(#45442,#45443),(#45444,#45445),
(#45446,#45447),(#45448,#45449),(#45450,#45451),(#45452,#45453),(#45454,
#45455),(#45456,#45457),(#45458,#45459),(#45460,#45461),(#45462,#45463),
(#45464,#45465),(#45466,#45467),(#45468,#45469),(#45470,#45471),(#45472,
#45473),(#45474,#45475),(#45476,#45477),(#45478,#45479),(#45480,#45481),
(#45482,#45483),(#45484,#45485),(#45486,#45487),(#45488,#45489),(#45490,
#45491),(#45492,#45493),(#45494,#45495),(#45496,#45497),(#45498,#45499),
(#45500,#45501),(#45502,#45503),(#45504,#45505),(#45506,#45507),(#45508,
#45509),(#45510,#45511),(#45512,#45513),(#45514,#45515),(#45516,#45517),
(#45518,#45519),(#45520,#45521),(#45522,#45523),(#45524,#45525),(#45526,
#45527),(#45528,#45529),(#45530,#45531),(#45532,#45533),(#45534,#45535),
(#45536,#45537),(#45538,#45539),(#45540,#45541),(#45542,#45543),(#45544,
#45545),(#45546,#45547),(#45548,#45549),(#45550,#45551),(#45552,#45553),
(#45554,#45555),(#45556,#45557),(#45558,#45559),(#45560,#45561),(#45562,
#45563),(#45564,#45565),(#45566,#45567),(#45568,#45569),(#45570,#45571),
(#45572,#45573),(#45574,#45575),(#45576,#45577),(#45578,#45579),(#45580,
#45581),(#45582,#45583),(#45584,#45585),(#45586,#45587),(#45588,#45589),
(#45590,#45591),(#45592,#45593),(#45594,#45595),(#45596,#45597),(#45598,
#45599),(#45600,#45601),(#45602,#45603),(#45604,#45605),(#45606,#45607),
(#45608,#45609),(#45610,#45611),(#45612,#45613),(#45614,#45615),(#45616,
#45617),(#45618,#45619),(#45620,#45621),(#45622,#45623),(#45624,#45625),
(#45626,#45627),(#45628,#45629),(#45630,#45631),(#45632,#45633),(#45634,
#45635),(#45636,#45637),(#45638,#45639),(#45640,#45641),(#45642,#45643),
(#45644,#45645),(#45646,#45647),(#45648,#45649),(#45650,#45651),(#45652,
#45653),(#45654,#45655),(#45656,#45657),(#45658,#45659),(#45660,#45661),
(#45662,#45663),(#45664,#45665),(#45666,#45667),(#45668,#45669),(#45670,
#45671),(#45672,#45673),(#45674,#45675),(#45676,#45677),(#45678,#45679),
(#45680,#45681),(#45682,#45683),(#45684,#45685),(#45686,#45687),(#45688,
#45689),(#45690,#45691),(#45692,#45693),(#45694,#45695),(#45696,#45697),
(#45698,#45699),(#45700,#45701),(#45702,#45703),(#45704,#45705),(#45706,
#45707),(#45708,#45709),(#45710,#45711),(#45712,#45713),(#45714,#45715),
(#45716,#45717),(#45718,#45719),(#45720,#45721),(#45722,#45723),(#45724,
#45725),(#45726,#45727),(#45728,#45729),(#45730,#45731),(#45732,#45733),
(#45734,#45735),(#45736,#45737),(#45738,#45739),(#45740,#45741),(#45742,
#45743),(#45744,#45745),(#45746,#45747),(#45748,#45749),(#45750,#45751),
(#45752,#45753),(#45754,#45755),(#45756,#45757),(#45758,#45759),(#45760,
#45761),(#45762,#45763),(#45764,#45765),(#45766,#45767),(#45768,#45769),
(#45770,#45771),(#45772,#45773),(#45774,#45775),(#45776,#45777),(#45778,
#45779),(#45780,#45781),(#45782,#45783),(#45784,#45785),(#45786,#45787),
(#45788,#45789),(#45790,#45791),(#45792,#45793),(#45794,#45795),(#45796,
#45797),(#45798,#45799),(#45800,#45801),(#45802,#45803),(#45804,#45805),
(#45806,#45807),(#45808,#45809),(#45810,#45811),(#45812,#45813),(#45814,
#45815),(#45816,#45817),(#45818,#45819),(#45820,#45821),(#45822,#45823),
(#45824,#45825),(#45826,#45827),(#45828,#45829),(#45830,#45831),(#45832,
#45833),(#45834,#45835),(#45836,#45837),(#45838,#45839),(#45840,#45841),
(#45842,#45843),(#45844,#45845),(#45846,#45847),(#45848,#45849),(#45850,
#45851),(#45852,#45853),(#45854,#45855),(#45856,#45857),(#45858,#45859),
(#45860,#45861),(#45862,#45863),(#45864,#45865),(#45866,#45867),(#45868,
#45869),(#45870,#45871),(#45872,#45873),(#45874,#45875),(#45876,#45877),
(#45878,#45879),(#45880,#45881),(#45882,#45883),(#45884,#45885),(#45886,
#45887),(#45888,#45889),(#45890,#45891),(#45892,#45893),(#45894,#45895),
(#45896,#45897),(#45898,#45899),(#45900,#45901),(#45902,#45903),(#45904,
#45905),(#45906,#45907),(#45908,#45909),(#45910,#45911),(#45912,#45913),
(#45914,#45915),(#45916,#45917),(#45918,#45919),(#45920,#45921),(#45922,
#45923),(#45924,#45925)),.UNSPECIFIED.,.F.,.F.,.F.)
B_SPLINE_SURFACE_WITH_KNOTS((6,1,1,1,1,1,1,1,1,1,1,1,1,1,1,1,1,1,1,1,1,
1,1,1,1,1,1,1,1,1,1,1,1,1,1,1,1,1,1,1,1,1,1,1,1,1,1,1,1,1,1,1,1,1,1,1,1,
1,1,1,1,1,1,1,1,1,1,1,1,1,1,1,1,1,1,1,1,1,1,1,1,1,1,1,1,1,1,1,1,1,1,1,1,
1,1,1,1,1,1,1,1,1,1,1,1,1,1,1,1,1,1,1,1,1,1,1,1,1,1,1,1,1,1,1,1,1,1,1,1,
1,1,1,1,1,1,1,1,1,1,1,1,1,1,1,1,1,1,1,1,1,1,1,1,1,1,1,1,1,1,1,1,1,1,1,1,
1,1,1,1,1,1,1,1,1,1,1,1,1,1,1,1,1,1,1,1,1,1,1,1,1,1,1,1,1,1,1,1,1,1,1,1,
1,1,1,1,1,1,1,1,1,1,1,1,1,1,1,1,1,1,1,1,1,1,1,1,1,1,1,1,1,1,1,1,1,1,1,1,
1,1,1,1,1,1,1,1,1,1,1,1,1,1,1,1,1,1,1,1,1,1,1,1,1,1,1,1,1,1,1,1,1,1,1,1,
1,1,1,1,1,1,1,1,1,1,1,1,1,1,1,1,1,1,1,1,1,1,1,1,1,1,1,1,1,1,1,1,1,1,1,1,
1,1,1,1,1,1,1,1,1,1,1,1,1,1,1,1,1,1,1,1,1,1,1,1,1,1,1,1,1,1,1,1,1,1,1,1,
1,1,1,1,1,1,1,1,1,1,1,1,1,1,1,6),(2,2),(0.,0.00277777777777778,0.00555555555555556,
0.00833333333333333,0.0111111111111111,0.0138888888888889,0.0166666666666667,
0.0194444444444444,0.0222222222222222,0.025,0.0277777777777778,0.0305555555555556,
0.0333333333333333,0.0361111111111111,0.0388888888888889,0.0416666666666667,
0.0444444444444444,0.0472222222222222,0.05,0.0527777777777778,0.0555555555555555,
0.0583333333333333,0.0611111111111111,0.0638888888888889,0.0666666666666666,
0.0694444444444444,0.0722222222222222,0.075,0.0777777777777778,0.0805555555555555,
0.0833333333333333,0.0861111111111111,0.0888888888888889,0.0916666666666667,
0.0944444444444445,0.0972222222222222,0.1,0.102777777777778,0.105555555555556,
0.108333333333333,0.111111111111111,0.113888888888889,0.116666666666667,
0.119444444444444,0.122222222222222,0.125,0.127777777777778,0.130555555555556,
0.133333333333333,0.136111111111111,0.138888888888889,0.141666666666667,
0.144444444444444,0.147222222222222,0.15,0.152777777777778,0.155555555555556,
0.158333333333333,0.161111111111111,0.163888888888889,0.166666666666667,
0.169444444444444,0.172222222222222,0.175,0.177777777777778,0.180555555555555,
0.183333333333333,0.186111111111111,0.188888888888889,0.191666666666666,
0.194444444444444,0.197222222222222,0.2,0.202777777777778,0.205555555555555,
0.208333333333333,0.211111111111111,0.213888888888889,0.216666666666666,
0.219444444444444,0.222222222222222,0.225,0.227777777777777,0.230555555555555,
0.233333333333333,0.236111111111111,0.238888888888889,0.241666666666666,
0.244444444444444,0.247222222222222,0.25,0.252777777777777,0.255555555555555,
0.258333333333333,0.261111111111111,0.263888888888888,0.266666666666666,
0.269444444444444,0.272222222222222,0.275,0.277777777777777,0.280555555555555,
0.283333333333333,0.286111111111111,0.288888888888888,0.291666666666666,
0.294444444444444,0.297222222222222,0.299999999999999,0.302777777777777,
0.305555555555555,0.308333333333333,0.311111111111111,0.313888888888888,
0.316666666666666,0.319444444444444,0.322222222222222,0.324999999999999,
0.327777777777777,0.330555555555555,0.333333333333333,0.33611111111111,
0.338888888888888,0.341666666666666,0.344444444444444,0.347222222222221,
0.349999999999999,0.352777777777777,0.355555555555555,0.358333333333333,
0.36111111111111,0.363888888888888,0.366666666666666,0.369444444444444,
0.372222222222221,0.374999999999999,0.377777777777777,0.380555555555555,
0.383333333333332,0.38611111111111,0.388888888888888,0.391666666666666,
0.394444444444444,0.397222222222221,0.399999999999999,0.402777777777777,
0.405555555555555,0.408333333333332,0.41111111111111,0.413888888888888,
0.416666666666666,0.419444444444443,0.422222222222221,0.424999999999999,
0.427777777777777,0.430555555555555,0.433333333333332,0.43611111111111,
0.438888888888888,0.441666666666666,0.444444444444443,0.447222222222221,
0.449999999999999,0.452777777777777,0.455555555555554,0.458333333333332,
0.46111111111111,0.463888888888888,0.466666666666666,0.469444444444443,
0.472222222222221,0.474999999999999,0.477777777777777,0.480555555555554,
0.483333333333332,0.48611111111111,0.488888888888888,0.491666666666665,
0.494444444444443,0.497222222222221,0.499999999999999,0.502777777777777,
0.505555555555554,0.508333333333332,0.51111111111111,0.513888888888888,
0.516666666666665,0.519444444444443,0.522222222222221,0.524999999999999,
0.527777777777776,0.530555555555554,0.533333333333332,0.53611111111111,
0.538888888888888,0.541666666666665,0.544444444444443,0.547222222222221,
0.549999999999999,0.552777777777776,0.555555555555554,0.558333333333332,
0.56111111111111,0.563888888888887,0.566666666666665,0.569444444444443,
0.572222222222221,0.574999999999999,0.577777777777776,0.580555555555554,
0.583333333333332,0.58611111111111,0.588888888888887,0.591666666666665,
0.594444444444443,0.597222222222221,0.599999999999998,0.602777777777776,
0.605555555555554,0.608333333333332,0.611111111111109,0.613888888888887,
0.616666666666665,0.619444444444443,0.622222222222221,0.624999999999998,
0.627777777777776,0.630555555555554,0.633333333333332,0.636111111111109,
0.638888888888887,0.641666666666665,0.644444444444443,0.64722222222222,
0.649999999999998,0.652777777777776,0.655555555555554,0.658333333333332,
0.661111111111109,0.663888888888887,0.666666666666665,0.669444444444443,
0.67222222222222,0.674999999999998,0.677777777777776,0.680555555555554,
0.683333333333331,0.686111111111109,0.688888888888887,0.691666666666665,
0.694444444444443,0.69722222222222,0.699999999999998,0.702777777777776,
0.705555555555554,0.708333333333331,0.711111111111109,0.713888888888887,
0.716666666666665,0.719444444444442,0.72222222222222,0.724999999999998,
0.727777777777776,0.730555555555554,0.733333333333331,0.736111111111109,
0.738888888888887,0.741666666666665,0.744444444444442,0.74722222222222,
0.749999999999998,0.752777777777776,0.755555555555553,0.758333333333331,
0.761111111111109,0.763888888888887,0.766666666666664,0.769444444444442,
0.77222222222222,0.774999999999998,0.777777777777776,0.780555555555553,
0.783333333333331,0.786111111111109,0.788888888888887,0.791666666666664,
0.794444444444442,0.79722222222222,0.799999999999998,0.802777777777775,
0.805555555555553,0.808333333333331,0.811111111111109,0.813888888888887,
0.816666666666664,0.819444444444442,0.82222222222222,0.824999999999998,
0.827777777777775,0.830555555555553,0.833333333333331,0.836111111111109,
0.838888888888886,0.841666666666664,0.844444444444442,0.84722222222222,
0.849999999999998,0.852777777777775,0.855555555555553,0.858333333333331,
0.861111111111109,0.863888888888886,0.866666666666664,0.869444444444442,
0.87222222222222,0.874999999999997,0.877777777777775,0.880555555555553,
0.883333333333331,0.886111111111109,0.888888888888886,0.891666666666664,
0.894444444444442,0.89722222222222,0.899999999999997,0.902777777777775,
0.905555555555553,0.908333333333331,0.911111111111108,0.913888888888886,
0.916666666666664,0.919444444444442,0.92222222222222,0.924999999999997,
0.927777777777775,0.930555555555553,0.933333333333331,0.936111111111108,
0.938888888888886,0.941666666666664,0.944444444444442,0.947222222222219,
0.949999999999997,0.952777777777775,0.955555555555553,0.95833333333333,
0.961111111111108,0.963888888888886,0.966666666666664,0.969444444444442,
0.972222222222219,0.974999999999997,0.977777777777775,0.980555555555553,
0.98333333333333,0.986111111111108,0.988888888888886,0.991666666666664,
0.994444444444441,0.997222222222219,1.),(0.,0.15),.UNSPECIFIED.)
GEOMETRIC_REPRESENTATION_ITEM()
RATIONAL_B_SPLINE_SURFACE(((1.,1.),(1.,1.),(1.,1.),(1.,1.),(1.,1.),(1.,
1.),(1.,1.),(1.,1.),(1.,1.),(1.,1.),(1.,1.),(1.,1.),(1.,1.),(1.,1.),(1.,
1.),(1.,1.),(1.,1.),(1.,1.),(1.,1.),(1.,1.),(1.,1.),(1.,1.),(1.,1.),(1.,
1.),(1.,1.),(1.,1.),(1.,1.),(1.,1.),(1.,1.),(1.,1.),(1.,1.),(1.,1.),(1.,
1.),(1.,1.),(1.,1.),(1.,1.),(1.,1.),(1.,1.),(1.,1.),(1.,1.),(1.,1.),(1.,
1.),(1.,1.),(1.,1.),(1.,1.),(1.,1.),(1.,1.),(1.,1.),(1.,1.),(1.,1.),(1.,
1.),(1.,1.),(1.,1.),(1.,1.),(1.,1.),(1.,1.),(1.,1.),(1.,1.),(1.,1.),(1.,
1.),(1.,1.),(1.,1.),(1.,1.),(1.,1.),(1.,1.),(1.,1.),(1.,1.),(1.,1.),(1.,
1.),(1.,1.),(1.,1.),(1.,1.),(1.,1.),(1.,1.),(1.,1.),(1.,1.),(1.,1.),(1.,
1.),(1.,1.),(1.,1.),(1.,1.),(1.,1.),(1.,1.),(1.,1.),(1.,1.),(1.,1.),(1.,
1.),(1.,1.),(1.,1.),(1.,1.),(1.,1.),(1.,1.),(1.,1.),(1.,1.),(1.,1.),(1.,
1.),(1.,1.),(1.,1.),(1.,1.),(1.,1.),(1.,1.),(1.,1.),(1.,1.),(1.,1.),(1.,
1.),(1.,1.),(1.,1.),(1.,1.),(1.,1.),(1.,1.),(1.,1.),(1.,1.),(1.,1.),(1.,
1.),(1.,1.),(1.,1.),(1.,1.),(1.,1.),(1.,1.),(1.,1.),(1.,1.),(1.,1.),(1.,
1.),(1.,1.),(1.,1.),(1.,1.),(1.,1.),(1.,1.),(1.,1.),(1.,1.),(1.,1.),(1.,
1.),(1.,1.),(1.,1.),(1.,1.),(1.,1.),(1.,1.),(1.,1.),(1.,1.),(1.,1.),(1.,
1.),(1.,1.),(1.,1.),(1.,1.),(1.,1.),(1.,1.),(1.,1.),(1.,1.),(1.,1.),(1.,
1.),(1.,1.),(1.,1.),(1.,1.),(1.,1.),(1.,1.),(1.,1.),(1.,1.),(1.,1.),(1.,
1.),(1.,1.),(1.,1.),(1.,1.),(1.,1.),(1.,1.),(1.,1.),(1.,1.),(1.,1.),(1.,
1.),(1.,1.),(1.,1.),(1.,1.),(1.,1.),(1.,1.),(1.,1.),(1.,1.),(1.,1.),(1.,
1.),(1.,1.),(1.,1.),(1.,1.),(1.,1.),(1.,1.),(1.,1.),(1.,1.),(1.,1.),(1.,
1.),(1.,1.),(1.,1.),(1.,1.),(1.,1.),(1.,1.),(1.,1.),(1.,1.),(1.,1.),(1.,
1.),(1.,1.),(1.,1.),(1.,1.),(1.,1.),(1.,1.),(1.,1.),(1.,1.),(1.,1.),(1.,
1.),(1.,1.),(1.,1.),(1.,1.),(1.,1.),(1.,1.),(1.,1.),(1.,1.),(1.,1.),(1.,
1.),(1.,1.),(1.,1.),(1.,1.),(1.,1.),(1.,1.),(1.,1.),(1.,1.),(1.,1.),(1.,
1.),(1.,1.),(1.,1.),(1.,1.),(1.,1.),(1.,1.),(1.,1.),(1.,1.),(1.,1.),(1.,
1.),(1.,1.),(1.,1.),(1.,1.),(1.,1.),(1.,1.),(1.,1.),(1.,1.),(1.,1.),(1.,
1.),(1.,1.),(1.,1.),(1.,1.),(1.,1.),(1.,1.),(1.,1.),(1.,1.),(1.,1.),(1.,
1.),(1.,1.),(1.,1.),(1.,1.),(1.,1.),(1.,1.),(1.,1.),(1.,1.),(1.,1.),(1.,
1.),(1.,1.),(1.,1.),(1.,1.),(1.,1.),(1.,1.),(1.,1.),(1.,1.),(1.,1.),(1.,
1.),(1.,1.),(1.,1.),(1.,1.),(1.,1.),(1.,1.),(1.,1.),(1.,1.),(1.,1.),(1.,
1.),(1.,1.),(1.,1.),(1.,1.),(1.,1.),(1.,1.),(1.,1.),(1.,1.),(1.,1.),(1.,
1.),(1.,1.),(1.,1.),(1.,1.),(1.,1.),(1.,1.),(1.,1.),(1.,1.),(1.,1.),(1.,
1.),(1.,1.),(1.,1.),(1.,1.),(1.,1.),(1.,1.),(1.,1.),(1.,1.),(1.,1.),(1.,
1.),(1.,1.),(1.,1.),(1.,1.),(1.,1.),(1.,1.),(1.,1.),(1.,1.),(1.,1.),(1.,
1.),(1.,1.),(1.,1.),(1.,1.),(1.,1.),(1.,1.),(1.,1.),(1.,1.),(1.,1.),(1.,
1.),(1.,1.),(1.,1.),(1.,1.),(1.,1.),(1.,1.),(1.,1.),(1.,1.),(1.,1.),(1.,
1.),(1.,1.),(1.,1.),(1.,1.),(1.,1.),(1.,1.),(1.,1.),(1.,1.),(1.,1.),(1.,
1.),(1.,1.),(1.,1.),(1.,1.),(1.,1.),(1.,1.),(1.,1.),(1.,1.),(1.,1.),(1.,
1.),(1.,1.),(1.,1.),(1.,1.),(1.,1.),(1.,1.),(1.,1.),(1.,1.),(1.,1.),(1.,
1.),(1.,1.),(1.,1.),(1.,1.),(1.,1.),(1.,1.),(1.,1.),(1.,1.),(1.,1.)))
REPRESENTATION_ITEM('')
SURFACE()
);
#1081=(
BOUNDED_SURFACE()
B_SPLINE_SURFACE(5,1,((#46179,#46180),(#46181,#46182),(#46183,#46184),(#46185,
#46186),(#46187,#46188),(#46189,#46190),(#46191,#46192),(#46193,#46194),
(#46195,#46196),(#46197,#46198),(#46199,#46200),(#46201,#46202),(#46203,
#46204),(#46205,#46206),(#46207,#46208),(#46209,#46210),(#46211,#46212),
(#46213,#46214),(#46215,#46216),(#46217,#46218),(#46219,#46220),(#46221,
#46222),(#46223,#46224),(#46225,#46226),(#46227,#46228),(#46229,#46230),
(#46231,#46232),(#46233,#46234),(#46235,#46236),(#46237,#46238),(#46239,
#46240),(#46241,#46242),(#46243,#46244),(#46245,#46246),(#46247,#46248),
(#46249,#46250),(#46251,#46252),(#46253,#46254),(#46255,#46256),(#46257,
#46258),(#46259,#46260),(#46261,#46262),(#46263,#46264),(#46265,#46266),
(#46267,#46268),(#46269,#46270),(#46271,#46272),(#46273,#46274),(#46275,
#46276),(#46277,#46278),(#46279,#46280),(#46281,#46282),(#46283,#46284),
(#46285,#46286),(#46287,#46288),(#46289,#46290),(#46291,#46292),(#46293,
#46294),(#46295,#46296),(#46297,#46298),(#46299,#46300),(#46301,#46302),
(#46303,#46304),(#46305,#46306),(#46307,#46308),(#46309,#46310),(#46311,
#46312),(#46313,#46314),(#46315,#46316),(#46317,#46318),(#46319,#46320),
(#46321,#46322),(#46323,#46324),(#46325,#46326),(#46327,#46328),(#46329,
#46330),(#46331,#46332),(#46333,#46334),(#46335,#46336),(#46337,#46338),
(#46339,#46340),(#46341,#46342),(#46343,#46344),(#46345,#46346),(#46347,
#46348),(#46349,#46350),(#46351,#46352),(#46353,#46354),(#46355,#46356),
(#46357,#46358),(#46359,#46360),(#46361,#46362),(#46363,#46364),(#46365,
#46366),(#46367,#46368),(#46369,#46370),(#46371,#46372),(#46373,#46374),
(#46375,#46376),(#46377,#46378),(#46379,#46380),(#46381,#46382),(#46383,
#46384),(#46385,#46386),(#46387,#46388),(#46389,#46390),(#46391,#46392),
(#46393,#46394),(#46395,#46396),(#46397,#46398),(#46399,#46400),(#46401,
#46402),(#46403,#46404),(#46405,#46406),(#46407,#46408),(#46409,#46410),
(#46411,#46412),(#46413,#46414),(#46415,#46416),(#46417,#46418),(#46419,
#46420),(#46421,#46422),(#46423,#46424),(#46425,#46426),(#46427,#46428),
(#46429,#46430),(#46431,#46432),(#46433,#46434),(#46435,#46436),(#46437,
#46438),(#46439,#46440),(#46441,#46442),(#46443,#46444),(#46445,#46446),
(#46447,#46448),(#46449,#46450),(#46451,#46452),(#46453,#46454),(#46455,
#46456),(#46457,#46458),(#46459,#46460),(#46461,#46462),(#46463,#46464),
(#46465,#46466),(#46467,#46468),(#46469,#46470),(#46471,#46472),(#46473,
#46474),(#46475,#46476),(#46477,#46478),(#46479,#46480),(#46481,#46482),
(#46483,#46484),(#46485,#46486),(#46487,#46488),(#46489,#46490),(#46491,
#46492),(#46493,#46494),(#46495,#46496),(#46497,#46498),(#46499,#46500),
(#46501,#46502),(#46503,#46504),(#46505,#46506),(#46507,#46508),(#46509,
#46510),(#46511,#46512),(#46513,#46514),(#46515,#46516),(#46517,#46518),
(#46519,#46520),(#46521,#46522),(#46523,#46524),(#46525,#46526),(#46527,
#46528),(#46529,#46530),(#46531,#46532),(#46533,#46534),(#46535,#46536),
(#46537,#46538),(#46539,#46540),(#46541,#46542),(#46543,#46544),(#46545,
#46546),(#46547,#46548),(#46549,#46550),(#46551,#46552),(#46553,#46554),
(#46555,#46556),(#46557,#46558),(#46559,#46560),(#46561,#46562),(#46563,
#46564),(#46565,#46566),(#46567,#46568),(#46569,#46570),(#46571,#46572),
(#46573,#46574),(#46575,#46576),(#46577,#46578),(#46579,#46580),(#46581,
#46582),(#46583,#46584),(#46585,#46586),(#46587,#46588),(#46589,#46590),
(#46591,#46592),(#46593,#46594),(#46595,#46596),(#46597,#46598),(#46599,
#46600),(#46601,#46602),(#46603,#46604),(#46605,#46606),(#46607,#46608),
(#46609,#46610),(#46611,#46612),(#46613,#46614),(#46615,#46616),(#46617,
#46618),(#46619,#46620),(#46621,#46622),(#46623,#46624),(#46625,#46626),
(#46627,#46628),(#46629,#46630),(#46631,#46632),(#46633,#46634),(#46635,
#46636),(#46637,#46638),(#46639,#46640),(#46641,#46642),(#46643,#46644),
(#46645,#46646),(#46647,#46648),(#46649,#46650),(#46651,#46652),(#46653,
#46654),(#46655,#46656),(#46657,#46658),(#46659,#46660),(#46661,#46662),
(#46663,#46664),(#46665,#46666),(#46667,#46668),(#46669,#46670),(#46671,
#46672),(#46673,#46674),(#46675,#46676),(#46677,#46678),(#46679,#46680),
(#46681,#46682),(#46683,#46684),(#46685,#46686),(#46687,#46688),(#46689,
#46690),(#46691,#46692),(#46693,#46694),(#46695,#46696),(#46697,#46698),
(#46699,#46700),(#46701,#46702),(#46703,#46704),(#46705,#46706),(#46707,
#46708),(#46709,#46710),(#46711,#46712),(#46713,#46714),(#46715,#46716),
(#46717,#46718),(#46719,#46720),(#46721,#46722),(#46723,#46724),(#46725,
#46726),(#46727,#46728),(#46729,#46730),(#46731,#46732),(#46733,#46734),
(#46735,#46736),(#46737,#46738),(#46739,#46740),(#46741,#46742),(#46743,
#46744),(#46745,#46746),(#46747,#46748),(#46749,#46750),(#46751,#46752),
(#46753,#46754),(#46755,#46756),(#46757,#46758),(#46759,#46760),(#46761,
#46762),(#46763,#46764),(#46765,#46766),(#46767,#46768),(#46769,#46770),
(#46771,#46772),(#46773,#46774),(#46775,#46776),(#46777,#46778),(#46779,
#46780),(#46781,#46782),(#46783,#46784),(#46785,#46786),(#46787,#46788),
(#46789,#46790),(#46791,#46792),(#46793,#46794),(#46795,#46796),(#46797,
#46798),(#46799,#46800),(#46801,#46802),(#46803,#46804),(#46805,#46806),
(#46807,#46808),(#46809,#46810),(#46811,#46812),(#46813,#46814),(#46815,
#46816),(#46817,#46818),(#46819,#46820),(#46821,#46822),(#46823,#46824),
(#46825,#46826),(#46827,#46828),(#46829,#46830),(#46831,#46832),(#46833,
#46834),(#46835,#46836),(#46837,#46838),(#46839,#46840),(#46841,#46842),
(#46843,#46844),(#46845,#46846),(#46847,#46848),(#46849,#46850),(#46851,
#46852),(#46853,#46854),(#46855,#46856),(#46857,#46858),(#46859,#46860),
(#46861,#46862),(#46863,#46864),(#46865,#46866),(#46867,#46868),(#46869,
#46870),(#46871,#46872),(#46873,#46874),(#46875,#46876),(#46877,#46878),
(#46879,#46880),(#46881,#46882),(#46883,#46884),(#46885,#46886),(#46887,
#46888),(#46889,#46890),(#46891,#46892),(#46893,#46894),(#46895,#46896),
(#46897,#46898),(#46899,#46900),(#46901,#46902),(#46903,#46904),(#46905,
#46906),(#46907,#46908)),.UNSPECIFIED.,.F.,.F.,.F.)
B_SPLINE_SURFACE_WITH_KNOTS((6,1,1,1,1,1,1,1,1,1,1,1,1,1,1,1,1,1,1,1,1,
1,1,1,1,1,1,1,1,1,1,1,1,1,1,1,1,1,1,1,1,1,1,1,1,1,1,1,1,1,1,1,1,1,1,1,1,
1,1,1,1,1,1,1,1,1,1,1,1,1,1,1,1,1,1,1,1,1,1,1,1,1,1,1,1,1,1,1,1,1,1,1,1,
1,1,1,1,1,1,1,1,1,1,1,1,1,1,1,1,1,1,1,1,1,1,1,1,1,1,1,1,1,1,1,1,1,1,1,1,
1,1,1,1,1,1,1,1,1,1,1,1,1,1,1,1,1,1,1,1,1,1,1,1,1,1,1,1,1,1,1,1,1,1,1,1,
1,1,1,1,1,1,1,1,1,1,1,1,1,1,1,1,1,1,1,1,1,1,1,1,1,1,1,1,1,1,1,1,1,1,1,1,
1,1,1,1,1,1,1,1,1,1,1,1,1,1,1,1,1,1,1,1,1,1,1,1,1,1,1,1,1,1,1,1,1,1,1,1,
1,1,1,1,1,1,1,1,1,1,1,1,1,1,1,1,1,1,1,1,1,1,1,1,1,1,1,1,1,1,1,1,1,1,1,1,
1,1,1,1,1,1,1,1,1,1,1,1,1,1,1,1,1,1,1,1,1,1,1,1,1,1,1,1,1,1,1,1,1,1,1,1,
1,1,1,1,1,1,1,1,1,1,1,1,1,1,1,1,1,1,1,1,1,1,1,1,1,1,1,1,1,1,1,1,1,1,1,1,
1,1,1,1,1,1,1,1,1,1,1,1,1,1,1,6),(2,2),(0.,0.00277777777777778,0.00555555555555556,
0.00833333333333333,0.0111111111111111,0.0138888888888889,0.0166666666666667,
0.0194444444444444,0.0222222222222222,0.025,0.0277777777777778,0.0305555555555556,
0.0333333333333333,0.0361111111111111,0.0388888888888889,0.0416666666666667,
0.0444444444444444,0.0472222222222222,0.05,0.0527777777777778,0.0555555555555555,
0.0583333333333333,0.0611111111111111,0.0638888888888889,0.0666666666666666,
0.0694444444444444,0.0722222222222222,0.075,0.0777777777777778,0.0805555555555555,
0.0833333333333333,0.0861111111111111,0.0888888888888889,0.0916666666666667,
0.0944444444444445,0.0972222222222222,0.1,0.102777777777778,0.105555555555556,
0.108333333333333,0.111111111111111,0.113888888888889,0.116666666666667,
0.119444444444444,0.122222222222222,0.125,0.127777777777778,0.130555555555556,
0.133333333333333,0.136111111111111,0.138888888888889,0.141666666666667,
0.144444444444444,0.147222222222222,0.15,0.152777777777778,0.155555555555556,
0.158333333333333,0.161111111111111,0.163888888888889,0.166666666666667,
0.169444444444444,0.172222222222222,0.175,0.177777777777778,0.180555555555555,
0.183333333333333,0.186111111111111,0.188888888888889,0.191666666666666,
0.194444444444444,0.197222222222222,0.2,0.202777777777778,0.205555555555555,
0.208333333333333,0.211111111111111,0.213888888888889,0.216666666666666,
0.219444444444444,0.222222222222222,0.225,0.227777777777777,0.230555555555555,
0.233333333333333,0.236111111111111,0.238888888888889,0.241666666666666,
0.244444444444444,0.247222222222222,0.25,0.252777777777777,0.255555555555555,
0.258333333333333,0.261111111111111,0.263888888888888,0.266666666666666,
0.269444444444444,0.272222222222222,0.275,0.277777777777777,0.280555555555555,
0.283333333333333,0.286111111111111,0.288888888888888,0.291666666666666,
0.294444444444444,0.297222222222222,0.299999999999999,0.302777777777777,
0.305555555555555,0.308333333333333,0.311111111111111,0.313888888888888,
0.316666666666666,0.319444444444444,0.322222222222222,0.324999999999999,
0.327777777777777,0.330555555555555,0.333333333333333,0.33611111111111,
0.338888888888888,0.341666666666666,0.344444444444444,0.347222222222221,
0.349999999999999,0.352777777777777,0.355555555555555,0.358333333333333,
0.36111111111111,0.363888888888888,0.366666666666666,0.369444444444444,
0.372222222222221,0.374999999999999,0.377777777777777,0.380555555555555,
0.383333333333332,0.38611111111111,0.388888888888888,0.391666666666666,
0.394444444444444,0.397222222222221,0.399999999999999,0.402777777777777,
0.405555555555555,0.408333333333332,0.41111111111111,0.413888888888888,
0.416666666666666,0.419444444444443,0.422222222222221,0.424999999999999,
0.427777777777777,0.430555555555555,0.433333333333332,0.43611111111111,
0.438888888888888,0.441666666666666,0.444444444444443,0.447222222222221,
0.449999999999999,0.452777777777777,0.455555555555554,0.458333333333332,
0.46111111111111,0.463888888888888,0.466666666666666,0.469444444444443,
0.472222222222221,0.474999999999999,0.477777777777777,0.480555555555554,
0.483333333333332,0.48611111111111,0.488888888888888,0.491666666666665,
0.494444444444443,0.497222222222221,0.499999999999999,0.502777777777777,
0.505555555555554,0.508333333333332,0.51111111111111,0.513888888888888,
0.516666666666665,0.519444444444443,0.522222222222221,0.524999999999999,
0.527777777777776,0.530555555555554,0.533333333333332,0.53611111111111,
0.538888888888888,0.541666666666665,0.544444444444443,0.547222222222221,
0.549999999999999,0.552777777777776,0.555555555555554,0.558333333333332,
0.56111111111111,0.563888888888887,0.566666666666665,0.569444444444443,
0.572222222222221,0.574999999999999,0.577777777777776,0.580555555555554,
0.583333333333332,0.58611111111111,0.588888888888887,0.591666666666665,
0.594444444444443,0.597222222222221,0.599999999999998,0.602777777777776,
0.605555555555554,0.608333333333332,0.611111111111109,0.613888888888887,
0.616666666666665,0.619444444444443,0.622222222222221,0.624999999999998,
0.627777777777776,0.630555555555554,0.633333333333332,0.636111111111109,
0.638888888888887,0.641666666666665,0.644444444444443,0.64722222222222,
0.649999999999998,0.652777777777776,0.655555555555554,0.658333333333332,
0.661111111111109,0.663888888888887,0.666666666666665,0.669444444444443,
0.67222222222222,0.674999999999998,0.677777777777776,0.680555555555554,
0.683333333333331,0.686111111111109,0.688888888888887,0.691666666666665,
0.694444444444443,0.69722222222222,0.699999999999998,0.702777777777776,
0.705555555555554,0.708333333333331,0.711111111111109,0.713888888888887,
0.716666666666665,0.719444444444442,0.72222222222222,0.724999999999998,
0.727777777777776,0.730555555555554,0.733333333333331,0.736111111111109,
0.738888888888887,0.741666666666665,0.744444444444442,0.74722222222222,
0.749999999999998,0.752777777777776,0.755555555555553,0.758333333333331,
0.761111111111109,0.763888888888887,0.766666666666664,0.769444444444442,
0.77222222222222,0.774999999999998,0.777777777777776,0.780555555555553,
0.783333333333331,0.786111111111109,0.788888888888887,0.791666666666664,
0.794444444444442,0.79722222222222,0.799999999999998,0.802777777777775,
0.805555555555553,0.808333333333331,0.811111111111109,0.813888888888887,
0.816666666666664,0.819444444444442,0.82222222222222,0.824999999999998,
0.827777777777775,0.830555555555553,0.833333333333331,0.836111111111109,
0.838888888888886,0.841666666666664,0.844444444444442,0.84722222222222,
0.849999999999998,0.852777777777775,0.855555555555553,0.858333333333331,
0.861111111111109,0.863888888888886,0.866666666666664,0.869444444444442,
0.87222222222222,0.874999999999997,0.877777777777775,0.880555555555553,
0.883333333333331,0.886111111111109,0.888888888888886,0.891666666666664,
0.894444444444442,0.89722222222222,0.899999999999997,0.902777777777775,
0.905555555555553,0.908333333333331,0.911111111111108,0.913888888888886,
0.916666666666664,0.919444444444442,0.92222222222222,0.924999999999997,
0.927777777777775,0.930555555555553,0.933333333333331,0.936111111111108,
0.938888888888886,0.941666666666664,0.944444444444442,0.947222222222219,
0.949999999999997,0.952777777777775,0.955555555555553,0.95833333333333,
0.961111111111108,0.963888888888886,0.966666666666664,0.969444444444442,
0.972222222222219,0.974999999999997,0.977777777777775,0.980555555555553,
0.98333333333333,0.986111111111108,0.988888888888886,0.991666666666664,
0.994444444444441,0.997222222222219,1.),(0.,0.15),.UNSPECIFIED.)
GEOMETRIC_REPRESENTATION_ITEM()
RATIONAL_B_SPLINE_SURFACE(((1.,1.),(1.,1.),(1.,1.),(1.,1.),(1.,1.),(1.,
1.),(1.,1.),(1.,1.),(1.,1.),(1.,1.),(1.,1.),(1.,1.),(1.,1.),(1.,1.),(1.,
1.),(1.,1.),(1.,1.),(1.,1.),(1.,1.),(1.,1.),(1.,1.),(1.,1.),(1.,1.),(1.,
1.),(1.,1.),(1.,1.),(1.,1.),(1.,1.),(1.,1.),(1.,1.),(1.,1.),(1.,1.),(1.,
1.),(1.,1.),(1.,1.),(1.,1.),(1.,1.),(1.,1.),(1.,1.),(1.,1.),(1.,1.),(1.,
1.),(1.,1.),(1.,1.),(1.,1.),(1.,1.),(1.,1.),(1.,1.),(1.,1.),(1.,1.),(1.,
1.),(1.,1.),(1.,1.),(1.,1.),(1.,1.),(1.,1.),(1.,1.),(1.,1.),(1.,1.),(1.,
1.),(1.,1.),(1.,1.),(1.,1.),(1.,1.),(1.,1.),(1.,1.),(1.,1.),(1.,1.),(1.,
1.),(1.,1.),(1.,1.),(1.,1.),(1.,1.),(1.,1.),(1.,1.),(1.,1.),(1.,1.),(1.,
1.),(1.,1.),(1.,1.),(1.,1.),(1.,1.),(1.,1.),(1.,1.),(1.,1.),(1.,1.),(1.,
1.),(1.,1.),(1.,1.),(1.,1.),(1.,1.),(1.,1.),(1.,1.),(1.,1.),(1.,1.),(1.,
1.),(1.,1.),(1.,1.),(1.,1.),(1.,1.),(1.,1.),(1.,1.),(1.,1.),(1.,1.),(1.,
1.),(1.,1.),(1.,1.),(1.,1.),(1.,1.),(1.,1.),(1.,1.),(1.,1.),(1.,1.),(1.,
1.),(1.,1.),(1.,1.),(1.,1.),(1.,1.),(1.,1.),(1.,1.),(1.,1.),(1.,1.),(1.,
1.),(1.,1.),(1.,1.),(1.,1.),(1.,1.),(1.,1.),(1.,1.),(1.,1.),(1.,1.),(1.,
1.),(1.,1.),(1.,1.),(1.,1.),(1.,1.),(1.,1.),(1.,1.),(1.,1.),(1.,1.),(1.,
1.),(1.,1.),(1.,1.),(1.,1.),(1.,1.),(1.,1.),(1.,1.),(1.,1.),(1.,1.),(1.,
1.),(1.,1.),(1.,1.),(1.,1.),(1.,1.),(1.,1.),(1.,1.),(1.,1.),(1.,1.),(1.,
1.),(1.,1.),(1.,1.),(1.,1.),(1.,1.),(1.,1.),(1.,1.),(1.,1.),(1.,1.),(1.,
1.),(1.,1.),(1.,1.),(1.,1.),(1.,1.),(1.,1.),(1.,1.),(1.,1.),(1.,1.),(1.,
1.),(1.,1.),(1.,1.),(1.,1.),(1.,1.),(1.,1.),(1.,1.),(1.,1.),(1.,1.),(1.,
1.),(1.,1.),(1.,1.),(1.,1.),(1.,1.),(1.,1.),(1.,1.),(1.,1.),(1.,1.),(1.,
1.),(1.,1.),(1.,1.),(1.,1.),(1.,1.),(1.,1.),(1.,1.),(1.,1.),(1.,1.),(1.,
1.),(1.,1.),(1.,1.),(1.,1.),(1.,1.),(1.,1.),(1.,1.),(1.,1.),(1.,1.),(1.,
1.),(1.,1.),(1.,1.),(1.,1.),(1.,1.),(1.,1.),(1.,1.),(1.,1.),(1.,1.),(1.,
1.),(1.,1.),(1.,1.),(1.,1.),(1.,1.),(1.,1.),(1.,1.),(1.,1.),(1.,1.),(1.,
1.),(1.,1.),(1.,1.),(1.,1.),(1.,1.),(1.,1.),(1.,1.),(1.,1.),(1.,1.),(1.,
1.),(1.,1.),(1.,1.),(1.,1.),(1.,1.),(1.,1.),(1.,1.),(1.,1.),(1.,1.),(1.,
1.),(1.,1.),(1.,1.),(1.,1.),(1.,1.),(1.,1.),(1.,1.),(1.,1.),(1.,1.),(1.,
1.),(1.,1.),(1.,1.),(1.,1.),(1.,1.),(1.,1.),(1.,1.),(1.,1.),(1.,1.),(1.,
1.),(1.,1.),(1.,1.),(1.,1.),(1.,1.),(1.,1.),(1.,1.),(1.,1.),(1.,1.),(1.,
1.),(1.,1.),(1.,1.),(1.,1.),(1.,1.),(1.,1.),(1.,1.),(1.,1.),(1.,1.),(1.,
1.),(1.,1.),(1.,1.),(1.,1.),(1.,1.),(1.,1.),(1.,1.),(1.,1.),(1.,1.),(1.,
1.),(1.,1.),(1.,1.),(1.,1.),(1.,1.),(1.,1.),(1.,1.),(1.,1.),(1.,1.),(1.,
1.),(1.,1.),(1.,1.),(1.,1.),(1.,1.),(1.,1.),(1.,1.),(1.,1.),(1.,1.),(1.,
1.),(1.,1.),(1.,1.),(1.,1.),(1.,1.),(1.,1.),(1.,1.),(1.,1.),(1.,1.),(1.,
1.),(1.,1.),(1.,1.),(1.,1.),(1.,1.),(1.,1.),(1.,1.),(1.,1.),(1.,1.),(1.,
1.),(1.,1.),(1.,1.),(1.,1.),(1.,1.),(1.,1.),(1.,1.),(1.,1.),(1.,1.),(1.,
1.),(1.,1.),(1.,1.),(1.,1.),(1.,1.),(1.,1.),(1.,1.),(1.,1.),(1.,1.),(1.,
1.),(1.,1.),(1.,1.),(1.,1.),(1.,1.),(1.,1.),(1.,1.),(1.,1.),(1.,1.),(1.,
1.),(1.,1.),(1.,1.),(1.,1.),(1.,1.),(1.,1.),(1.,1.),(1.,1.),(1.,1.)))
REPRESENTATION_ITEM('')
SURFACE()
);
#1300=STYLED_ITEM('',(#60513),#92);
#1885=FACE_OUTER_BOUND('',#2893,.T.);
#1886=FACE_OUTER_BOUND('',#2894,.T.);
#1887=FACE_OUTER_BOUND('',#2895,.T.);
#1888=FACE_OUTER_BOUND('',#2896,.T.);
#1889=FACE_OUTER_BOUND('',#2897,.T.);
#1890=FACE_OUTER_BOUND('',#2898,.T.);
#1891=FACE_OUTER_BOUND('',#2899,.T.);
#1892=FACE_OUTER_BOUND('',#2900,.T.);
#1893=FACE_OUTER_BOUND('',#2901,.T.);
#1894=FACE_OUTER_BOUND('',#2902,.T.);
#2893=EDGE_LOOP('',(#14983,#14984,#14985,#14986));
#2894=EDGE_LOOP('',(#14987,#14988,#14989,#14990,#14991,#14992,#14993,#14994));
#2895=EDGE_LOOP('',(#14995,#14996,#14997,#14998));
#2896=EDGE_LOOP('',(#14999,#15000,#15001,#15002));
#2897=EDGE_LOOP('',(#15003,#15004,#15005,#15006));
#2898=EDGE_LOOP('',(#15007,#15008,#15009,#15010));
#2899=EDGE_LOOP('',(#15011,#15012,#15013,#15014));
#2900=EDGE_LOOP('',(#15015,#15016,#15017,#15018,#15019,#15020,#15021,#15022));
#2901=EDGE_LOOP('',(#15023,#15024,#15025,#15026));
#2902=EDGE_LOOP('',(#15027,#15028,#15029,#15030));
#4103=B_SPLINE_CURVE_WITH_KNOTS('',3,(#45131,#45132,#45133,#45134),
 .UNSPECIFIED.,.F.,.F.,(4,4),(-1.,0.),.UNSPECIFIED.);
#4104=B_SPLINE_CURVE_WITH_KNOTS('',3,(#45136,#45137,#45138,#45139,#45140,
#45141,#45142,#45143,#45144,#45145,#45146,#45147,#45148,#45149),
 .UNSPECIFIED.,.F.,.F.,(4,1,1,1,1,1,1,1,1,1,1,4),(-0.999999865868381,-0.914814814814814,
-0.829629629629628,-0.744444444444442,-0.619444444444443,-0.504629629629628,
-0.389814814814814,-0.275,-0.266666666666666,-0.177777777777777,-0.0888888888888885,
-2.68263378817682E-7),.UNSPECIFIED.);
#4105=B_SPLINE_CURVE_WITH_KNOTS('',3,(#45151,#45152,#45153,#45154),
 .UNSPECIFIED.,.F.,.F.,(4,4),(0.,0.0212132034459712),.UNSPECIFIED.);
#4106=B_SPLINE_CURVE_WITH_KNOTS('',3,(#45155,#45156,#45157,#45158,#45159,
#45160,#45161,#45162,#45163,#45164,#45165,#45166,#45167,#45168),
 .UNSPECIFIED.,.F.,.F.,(4,1,1,1,1,1,1,1,1,1,1,4),(-3.29679099043599E-16,
0.0888888888888885,0.177777777777777,0.266666666666666,0.275,0.389814814814814,
0.504629629629628,0.619444444444443,0.744444444444442,0.829629629629628,
0.914814814814814,1.),.UNSPECIFIED.);
#4107=B_SPLINE_CURVE_WITH_KNOTS('',3,(#45173,#45174,#45175,#45176),
 .UNSPECIFIED.,.F.,.F.,(4,4),(-1.,0.),.UNSPECIFIED.);
#4108=B_SPLINE_CURVE_WITH_KNOTS('',3,(#45180,#45181,#45182,#45183,#45184,
#45185),.UNSPECIFIED.,.F.,.F.,(4,2,4),(0.,0.0106066017228885,0.0212132034457774),
 .UNSPECIFIED.);
#4109=B_SPLINE_CURVE_WITH_KNOTS('',3,(#45189,#45190,#45191,#45192,#45193,
#45194),.UNSPECIFIED.,.F.,.F.,(4,2,4),(0.,0.0106066017228885,0.0212132034457775),
 .UNSPECIFIED.);
#4110=B_SPLINE_CURVE_WITH_KNOTS('',3,(#45928,#45929,#45930,#45931,#45932,
#45933,#45934,#45935,#45936,#45937,#45938,#45939,#45940,#45941),
 .UNSPECIFIED.,.F.,.F.,(4,1,1,1,1,1,1,1,1,1,1,4),(-0.999999865868361,-0.914814725393722,
-0.829629584919082,-0.744444444444442,-0.619444444444443,-0.504629629629628,
-0.389814814814814,-0.275,-0.266666666666666,-0.177777777777776,-0.0888888888888856,
4.77815499535063E-15),.UNSPECIFIED.);
#4111=B_SPLINE_CURVE_WITH_KNOTS('',3,(#45999,#46000,#46001,#46002),
 .UNSPECIFIED.,.F.,.F.,(4,4),(0.,0.0212132034459714),.UNSPECIFIED.);
#4112=B_SPLINE_CURVE_WITH_KNOTS('',3,(#46003,#46004,#46005,#46006,#46007,
#46008,#46009,#46010,#46011,#46012,#46013,#46014,#46015,#46016),
 .UNSPECIFIED.,.F.,.F.,(4,1,1,1,1,1,1,1,1,1,1,4),(1.3413170185661E-7,0.0888888888888856,
0.177777777777776,0.266666666666666,0.275,0.389814814814814,0.504629629629628,
0.619444444444443,0.744444444444442,0.829629584919082,0.914814725393722,
0.999999865868361),.UNSPECIFIED.);
#4113=B_SPLINE_CURVE_WITH_KNOTS('',3,(#46123,#46124,#46125,#46126),
 .UNSPECIFIED.,.F.,.F.,(4,4),(-1.,0.),.UNSPECIFIED.);
#4114=B_SPLINE_CURVE_WITH_KNOTS('',3,(#46127,#46128,#46129,#46130,#46131,
#46132,#46133,#46134,#46135,#46136,#46137,#46138,#46139,#46140,#46141,#46142,
#46143,#46144,#46145,#46146,#46147,#46148,#46149,#46150,#46151,#46152),
 .UNSPECIFIED.,.F.,.F.,(4,1,1,1,1,1,1,1,1,1,1,1,1,1,1,1,1,1,1,1,1,1,1,4),
(-1.,-0.988888888888886,-0.969444444444442,-0.856944444444442,-0.744444444444442,
-0.688888888888887,-0.686111111111109,-0.658333333333332,-0.644444444444443,
-0.547222222222221,-0.466666666666666,-0.433333333333332,-0.36111111111111,
-0.277777777777777,-0.218055555555555,-0.158333333333333,-0.15,-0.147222222222222,
-0.130555555555556,-0.105555555555556,-0.102777777777778,-0.05,-0.00277777777777778,
1.52611180263545E-7),.UNSPECIFIED.);
#4115=B_SPLINE_CURVE_WITH_KNOTS('',3,(#46153,#46154,#46155,#46156,#46157,
#46158,#46159,#46160,#46161,#46162,#46163,#46164,#46165,#46166,#46167,#46168,
#46169,#46170,#46171,#46172,#46173,#46174,#46175,#46176,#46177,#46178),
 .UNSPECIFIED.,.F.,.F.,(4,1,1,1,1,1,1,1,1,1,1,1,1,1,1,1,1,1,1,1,1,1,1,4),
(-2.64697796016969E-23,0.00277777777777778,0.05,0.102777777777778,0.105555555555556,
0.130555555555556,0.147222222222222,0.15,0.158333333333333,0.218055555555555,
0.277777777777777,0.36111111111111,0.433333333333332,0.466666666666666,
0.547222222222221,0.644444444444443,0.658333333333332,0.686111111111109,
0.688888888888887,0.744444444444442,0.856944444444442,0.969444444444442,
0.988888888888886,1.),.UNSPECIFIED.);
#4116=B_SPLINE_CURVE_WITH_KNOTS('',3,(#46910,#46911,#46912,#46913,#46914,
#46915,#46916,#46917,#46918,#46919,#46920,#46921,#46922,#46923,#46924,#46925,
#46926,#46927,#46928,#46929,#46930,#46931,#46932,#46933),.UNSPECIFIED.,
 .F.,.F.,(4,1,1,1,1,1,1,1,1,1,1,1,1,1,1,1,1,1,1,1,1,4),(-1.,-0.988888888888886,
-0.969444444444442,-0.856944444444442,-0.744444444444442,-0.688888888888887,
-0.686111111111109,-0.658333333333332,-0.644444444444443,-0.547222222222221,
-0.466666666666666,-0.433333333333332,-0.36111111111111,-0.277777777777777,
-0.218055555555555,-0.158333333333333,-0.15,-0.147222222222222,-0.105555555555556,
-0.0527777777777778,-0.05,-1.52611156942486E-7),.UNSPECIFIED.);
#4117=B_SPLINE_CURVE_WITH_KNOTS('',3,(#47032,#47033,#47034,#47035),
 .UNSPECIFIED.,.F.,.F.,(4,4),(-1.,0.),.UNSPECIFIED.);
#4118=B_SPLINE_CURVE_WITH_KNOTS('',3,(#47036,#47037,#47038,#47039,#47040,
#47041,#47042,#47043,#47044,#47045,#47046,#47047,#47048,#47049,#47050,#47051,
#47052,#47053,#47054,#47055,#47056,#47057,#47058,#47059),.UNSPECIFIED.,
 .F.,.F.,(4,1,1,1,1,1,1,1,1,1,1,1,1,1,1,1,1,1,1,1,1,4),(-1.52611180304074E-7,
0.05,0.0527777777777778,0.105555555555556,0.147222222222222,0.15,0.158333333333333,
0.218055555555555,0.277777777777777,0.36111111111111,0.433333333333332,
0.466666666666666,0.547222222222221,0.644444444444443,0.658333333333332,
0.686111111111109,0.688888888888887,0.744444444444442,0.856944444444442,
0.969444444444442,0.988888888888886,1.),.UNSPECIFIED.);
#5340=LINE('',#45171,#6752);
#5341=LINE('',#45178,#6753);
#5342=LINE('',#45187,#6754);
#5343=LINE('',#45195,#6755);
#5344=LINE('',#45927,#6756);
#5345=LINE('',#46934,#6757);
#5346=LINE('',#47061,#6758);
#5347=LINE('',#47062,#6759);
#6752=VECTOR('',#22138,10.);
#6753=VECTOR('',#22139,10.);
#6754=VECTOR('',#22140,10.);
#6755=VECTOR('',#22141,10.);
#6756=VECTOR('',#22142,10.);
#6757=VECTOR('',#22143,10.);
#6758=VECTOR('',#22146,10.);
#6759=VECTOR('',#22147,10.);
#8368=VERTEX_POINT('',#45129);
#8369=VERTEX_POINT('',#45130);
#8370=VERTEX_POINT('',#45135);
#8371=VERTEX_POINT('',#45150);
#8372=VERTEX_POINT('',#45170);
#8373=VERTEX_POINT('',#45172);
#8374=VERTEX_POINT('',#45177);
#8375=VERTEX_POINT('',#45179);
#8376=VERTEX_POINT('',#45186);
#8377=VERTEX_POINT('',#45188);
#8378=VERTEX_POINT('',#45926);
#8379=VERTEX_POINT('',#45998);
#8380=VERTEX_POINT('',#46121);
#8381=VERTEX_POINT('',#46122);
#8382=VERTEX_POINT('',#46909);
#8383=VERTEX_POINT('',#47031);
#10699=EDGE_CURVE('',#8368,#8369,#4103,.T.);
#10700=EDGE_CURVE('',#8369,#8370,#4104,.T.);
#10701=EDGE_CURVE('',#8370,#8371,#4105,.T.);
#10702=EDGE_CURVE('',#8371,#8368,#4106,.T.);
#10703=EDGE_CURVE('',#8372,#8368,#5340,.T.);
#10704=EDGE_CURVE('',#8373,#8372,#4107,.T.);
#10705=EDGE_CURVE('',#8373,#8374,#5341,.T.);
#10706=EDGE_CURVE('',#8375,#8374,#4108,.T.);
#10707=EDGE_CURVE('',#8375,#8376,#5342,.T.);
#10708=EDGE_CURVE('',#8377,#8376,#4109,.T.);
#10709=EDGE_CURVE('',#8369,#8377,#5343,.T.);
#10710=EDGE_CURVE('',#8378,#8371,#5344,.T.);
#10711=EDGE_CURVE('',#8372,#8378,#4110,.T.);
#10712=EDGE_CURVE('',#8378,#8379,#4111,.T.);
#10713=EDGE_CURVE('',#8379,#8373,#4112,.T.);
#10714=EDGE_CURVE('',#8380,#8381,#4113,.T.);
#10715=EDGE_CURVE('',#8381,#8377,#4114,.T.);
#10716=EDGE_CURVE('',#8376,#8380,#4115,.T.);
#10717=EDGE_CURVE('',#8382,#8375,#4116,.T.);
#10718=EDGE_CURVE('',#8382,#8380,#5345,.T.);
#10719=EDGE_CURVE('',#8383,#8382,#4117,.T.);
#10720=EDGE_CURVE('',#8374,#8383,#4118,.T.);
#10721=EDGE_CURVE('',#8381,#8370,#5346,.T.);
#10722=EDGE_CURVE('',#8383,#8379,#5347,.T.);
#14983=ORIENTED_EDGE('',*,*,#10699,.T.);
#14984=ORIENTED_EDGE('',*,*,#10700,.T.);
#14985=ORIENTED_EDGE('',*,*,#10701,.T.);
#14986=ORIENTED_EDGE('',*,*,#10702,.T.);
#14987=ORIENTED_EDGE('',*,*,#10699,.F.);
#14988=ORIENTED_EDGE('',*,*,#10703,.F.);
#14989=ORIENTED_EDGE('',*,*,#10704,.F.);
#14990=ORIENTED_EDGE('',*,*,#10705,.T.);
#14991=ORIENTED_EDGE('',*,*,#10706,.F.);
#14992=ORIENTED_EDGE('',*,*,#10707,.T.);
#14993=ORIENTED_EDGE('',*,*,#10708,.F.);
#14994=ORIENTED_EDGE('',*,*,#10709,.F.);
#14995=ORIENTED_EDGE('',*,*,#10702,.F.);
#14996=ORIENTED_EDGE('',*,*,#10710,.F.);
#14997=ORIENTED_EDGE('',*,*,#10711,.F.);
#14998=ORIENTED_EDGE('',*,*,#10703,.T.);
#14999=ORIENTED_EDGE('',*,*,#10704,.T.);
#15000=ORIENTED_EDGE('',*,*,#10711,.T.);
#15001=ORIENTED_EDGE('',*,*,#10712,.T.);
#15002=ORIENTED_EDGE('',*,*,#10713,.T.);
#15003=ORIENTED_EDGE('',*,*,#10714,.T.);
#15004=ORIENTED_EDGE('',*,*,#10715,.T.);
#15005=ORIENTED_EDGE('',*,*,#10708,.T.);
#15006=ORIENTED_EDGE('',*,*,#10716,.T.);
#15007=ORIENTED_EDGE('',*,*,#10716,.F.);
#15008=ORIENTED_EDGE('',*,*,#10707,.F.);
#15009=ORIENTED_EDGE('',*,*,#10717,.F.);
#15010=ORIENTED_EDGE('',*,*,#10718,.T.);
#15011=ORIENTED_EDGE('',*,*,#10719,.T.);
#15012=ORIENTED_EDGE('',*,*,#10717,.T.);
#15013=ORIENTED_EDGE('',*,*,#10706,.T.);
#15014=ORIENTED_EDGE('',*,*,#10720,.T.);
#15015=ORIENTED_EDGE('',*,*,#10701,.F.);
#15016=ORIENTED_EDGE('',*,*,#10721,.F.);
#15017=ORIENTED_EDGE('',*,*,#10714,.F.);
#15018=ORIENTED_EDGE('',*,*,#10718,.F.);
#15019=ORIENTED_EDGE('',*,*,#10719,.F.);
#15020=ORIENTED_EDGE('',*,*,#10722,.T.);
#15021=ORIENTED_EDGE('',*,*,#10712,.F.);
#15022=ORIENTED_EDGE('',*,*,#10710,.T.);
#15023=ORIENTED_EDGE('',*,*,#10700,.F.);
#15024=ORIENTED_EDGE('',*,*,#10709,.T.);
#15025=ORIENTED_EDGE('',*,*,#10715,.F.);
#15026=ORIENTED_EDGE('',*,*,#10721,.T.);
#15027=ORIENTED_EDGE('',*,*,#10713,.F.);
#15028=ORIENTED_EDGE('',*,*,#10722,.F.);
#15029=ORIENTED_EDGE('',*,*,#10720,.F.);
#15030=ORIENTED_EDGE('',*,*,#10705,.F.);
#17913=ADVANCED_FACE('',(#1885),#127,.T.);
#17914=ADVANCED_FACE('',(#1886),#604,.T.);
#17915=ADVANCED_FACE('',(#1887),#1080,.T.);
#17916=ADVANCED_FACE('',(#1888),#128,.T.);
#17917=ADVANCED_FACE('',(#1889),#129,.T.);
#17918=ADVANCED_FACE('',(#1890),#1081,.T.);
#17919=ADVANCED_FACE('',(#1891),#130,.T.);
#17920=ADVANCED_FACE('',(#1892),#605,.T.);
#17921=ADVANCED_FACE('',(#1893),#606,.T.);
#17922=ADVANCED_FACE('',(#1894),#607,.F.);
#18302=CLOSED_SHELL('',(#17913,#17914,#17915,#17916,#17917,#17918,#17919,
#17920,#17921,#17922));
#19226=AXIS2_PLACEMENT_3D('',#45072,#22134,#22135);
#19227=AXIS2_PLACEMENT_3D('',#45169,#22136,#22137);
#19228=AXIS2_PLACEMENT_3D('',#47060,#22144,#22145);
#19229=AXIS2_PLACEMENT_3D('',#47063,#22148,#22149);
#19230=AXIS2_PLACEMENT_3D('',#47064,#22150,#22151);
#22134=DIRECTION('axis',(0.,0.,1.));
#22135=DIRECTION('refdir',(1.,0.,0.));
#22136=DIRECTION('center_axis',(0.,0.024997395914712,0.999687516275703));
#22137=DIRECTION('ref_axis',(0.,-0.999687516275703,0.024997395914712));
#22138=DIRECTION('',(1.,0.,0.));
#22139=DIRECTION('',(0.,-0.999687516275703,0.024997395914712));
#22140=DIRECTION('',(1.,0.,0.));
#22141=DIRECTION('',(0.,-0.999687516275703,0.024997395914712));
#22142=DIRECTION('',(1.,0.,0.));
#22143=DIRECTION('',(1.,0.,0.));
#22144=DIRECTION('center_axis',(0.,0.0249973959147123,-0.999687516275703));
#22145=DIRECTION('ref_axis',(0.,0.999687516275703,0.0249973959147123));
#22146=DIRECTION('',(0.,0.999687516275703,0.0249973959147123));
#22147=DIRECTION('',(0.,0.999687516275703,0.0249973959147123));
#22148=DIRECTION('center_axis',(1.,0.,0.));
#22149=DIRECTION('ref_axis',(0.,0.,-1.));
#22150=DIRECTION('center_axis',(1.,0.,0.));
#22151=DIRECTION('ref_axis',(0.,0.,-1.));
#45072=CARTESIAN_POINT('',(0.,0.,0.));
#45073=CARTESIAN_POINT('Ctrl Pts',(1.5,7.84754716719688,0.196222987756156));
#45074=CARTESIAN_POINT('Ctrl Pts',(1.5,7.81119228460987,1.64757063353881));
#45075=CARTESIAN_POINT('Ctrl Pts',(1.5,6.91554447525315,4.51998492486374));
#45076=CARTESIAN_POINT('Ctrl Pts',(1.5,3.50267736434437,7.4868718005881));
#45077=CARTESIAN_POINT('Ctrl Pts',(1.5,0.388976709839364,7.98738647591309));
#45078=CARTESIAN_POINT('Ctrl Pts',(1.5,-3.03605598459972,7.49963380638162));
#45079=CARTESIAN_POINT('Ctrl Pts',(1.5,-6.61228876173712,5.42165566355736));
#45080=CARTESIAN_POINT('Ctrl Pts',(1.5,-8.54932617078778,-0.243176633643623));
#45081=CARTESIAN_POINT('Ctrl Pts',(1.5,-6.22283392853507,-5.96728243109739));
#45082=CARTESIAN_POINT('Ctrl Pts',(1.5,-1.04981238929058,-8.37823413619139));
#45083=CARTESIAN_POINT('Ctrl Pts',(1.5,3.83069172671807,-7.27968997349867));
#45084=CARTESIAN_POINT('Ctrl Pts',(1.5,6.98760878535643,-4.34429198533913));
#45085=CARTESIAN_POINT('Ctrl Pts',(1.5,7.81270707141321,-1.58709781495809));
#45086=CARTESIAN_POINT('Ctrl Pts',(1.5,7.8475471671968,-0.196222987759265));
#45087=CARTESIAN_POINT('Ctrl Pts',(1.45,7.8975314881998,0.197475047609996));
#45088=CARTESIAN_POINT('Ctrl Pts',(1.45,7.86096333275704,1.6580604328562));
#45089=CARTESIAN_POINT('Ctrl Pts',(1.45,6.9595908976357,4.54876633855873));
#45090=CARTESIAN_POINT('Ctrl Pts',(1.45,3.52498432623248,7.53457411142355));
#45091=CARTESIAN_POINT('Ctrl Pts',(1.45,0.391454182214871,8.03823003379014));
#45092=CARTESIAN_POINT('Ctrl Pts',(1.45,-3.05539276487285,7.54742851941855));
#45093=CARTESIAN_POINT('Ctrl Pts',(1.45,-6.65440676033426,5.45617725481441));
#45094=CARTESIAN_POINT('Ctrl Pts',(1.45,-8.60378192629141,-0.244722612287108));
#45095=CARTESIAN_POINT('Ctrl Pts',(1.45,-6.26246888682433,-6.00528658546585));
#45096=CARTESIAN_POINT('Ctrl Pts',(1.45,-1.05649900580092,-8.43160864942561));
#45097=CARTESIAN_POINT('Ctrl Pts',(1.45,3.85509473392834,-7.32602697005844));
#45098=CARTESIAN_POINT('Ctrl Pts',(1.45,7.03210632247969,-4.37199570838387));
#45099=CARTESIAN_POINT('Ctrl Pts',(1.45,7.86249342936929,-1.59716926962579));
#45100=CARTESIAN_POINT('Ctrl Pts',(1.45,7.89753148819974,-0.197475047612075));
#45101=CARTESIAN_POINT('Ctrl Pts',(1.4,7.94751580920271,0.198727107463835));
#45102=CARTESIAN_POINT('Ctrl Pts',(1.39999999999993,7.91068240791007,1.66845448860209));
#45103=CARTESIAN_POINT('Ctrl Pts',(1.40000000000002,7.00364385267458,4.57759399919538));
#45104=CARTESIAN_POINT('Ctrl Pts',(1.39999999999998,3.54730042414692,7.58220147330159));
#45105=CARTESIAN_POINT('Ctrl Pts',(1.40000000000001,0.393932018706067,8.08916896201712));
#45106=CARTESIAN_POINT('Ctrl Pts',(1.4,-3.07473297912541,7.59514305847378));
#45107=CARTESIAN_POINT('Ctrl Pts',(1.4,-6.69652021371548,5.49073393546304));
#45108=CARTESIAN_POINT('Ctrl Pts',(1.4,-8.65823334930758,-0.246279305382362));
#45109=CARTESIAN_POINT('Ctrl Pts',(1.4,-6.30210657736778,-6.04329867241492));
#45110=CARTESIAN_POINT('Ctrl Pts',(1.4,-1.06318590207245,-8.48495865972949));
#45111=CARTESIAN_POINT('Ctrl Pts',(1.4,3.87948701006332,-7.37243510096405));
#45112=CARTESIAN_POINT('Ctrl Pts',(1.4,7.07663300474131,-4.39961875654197));
#45113=CARTESIAN_POINT('Ctrl Pts',(1.4,7.91221070955278,-1.60724928656839));
#45114=CARTESIAN_POINT('Ctrl Pts',(1.4,7.94751580920268,-0.198727107464886));
#45115=CARTESIAN_POINT('Ctrl Pts',(1.35,7.99750013020562,0.199979167317675));
#45116=CARTESIAN_POINT('Ctrl Pts',(1.34999999999993,7.96045345605724,1.67894428791948));
#45117=CARTESIAN_POINT('Ctrl Pts',(1.35000000000002,7.04769027505713,4.60637541289036));
#45118=CARTESIAN_POINT('Ctrl Pts',(1.34999999999998,3.56960738603504,7.62990378413704));
#45119=CARTESIAN_POINT('Ctrl Pts',(1.35000000000001,0.396409491081574,8.14001251989417));
#45120=CARTESIAN_POINT('Ctrl Pts',(1.35,-3.09406975939854,7.6429377715107));
#45121=CARTESIAN_POINT('Ctrl Pts',(1.35,-6.73863821231263,5.52525552672008));
#45122=CARTESIAN_POINT('Ctrl Pts',(1.35,-8.71268910481122,-0.247825284025847));
#45123=CARTESIAN_POINT('Ctrl Pts',(1.35,-6.34174153565703,-6.08130282678338));
#45124=CARTESIAN_POINT('Ctrl Pts',(1.35,-1.06987251858278,-8.53833317296371));
#45125=CARTESIAN_POINT('Ctrl Pts',(1.35,3.9038900172736,-7.41877209752381));
#45126=CARTESIAN_POINT('Ctrl Pts',(1.35,7.12113054186457,-4.42732247958672));
#45127=CARTESIAN_POINT('Ctrl Pts',(1.35,7.96199706750886,-1.61732074123609));
#45128=CARTESIAN_POINT('Ctrl Pts',(1.35,7.99750013020562,-0.199979167317696));
#45129=CARTESIAN_POINT('',(1.35,7.99750013020562,-0.199979167317696));
#45130=CARTESIAN_POINT('',(1.5,7.84754700261759,-0.196229557926748));
#45131=CARTESIAN_POINT('Ctrl Pts',(1.35,7.99750013020562,-0.199979167317696));
#45132=CARTESIAN_POINT('Ctrl Pts',(1.4,7.94751580920268,-0.198727107464886));
#45133=CARTESIAN_POINT('Ctrl Pts',(1.45,7.89753148819974,-0.197475047612075));
#45134=CARTESIAN_POINT('Ctrl Pts',(1.5,7.8475471671968,-0.196222987759265));
#45135=CARTESIAN_POINT('',(1.5,7.8475470026176,0.196229557926727));
#45136=CARTESIAN_POINT('Ctrl Pts',(1.5,7.84754700261754,-0.196229557925989));
#45137=CARTESIAN_POINT('Ctrl Pts',(1.5,7.81270577222208,-1.58710215640402));
#45138=CARTESIAN_POINT('Ctrl Pts',(1.5,6.98760712840792,-4.3442935260205));
#45139=CARTESIAN_POINT('Ctrl Pts',(1.5,3.83069172671807,-7.27968997349867));
#45140=CARTESIAN_POINT('Ctrl Pts',(1.5,-1.04981238929058,-8.37823413619139));
#45141=CARTESIAN_POINT('Ctrl Pts',(1.5,-6.22283392853507,-5.96728243109739));
#45142=CARTESIAN_POINT('Ctrl Pts',(1.5,-8.54932617078778,-0.243176633643623));
#45143=CARTESIAN_POINT('Ctrl Pts',(1.5,-6.61228876173712,5.42165566355736));
#45144=CARTESIAN_POINT('Ctrl Pts',(1.5,-3.03605598459972,7.49963380638162));
#45145=CARTESIAN_POINT('Ctrl Pts',(1.5,0.388976709839364,7.98738647591309));
#45146=CARTESIAN_POINT('Ctrl Pts',(1.5,3.50267736434437,7.4868718005881));
#45147=CARTESIAN_POINT('Ctrl Pts',(1.5,6.91554104195091,4.51998790951536));
#45148=CARTESIAN_POINT('Ctrl Pts',(1.5,7.81118958157476,1.64757930237687));
#45149=CARTESIAN_POINT('Ctrl Pts',(1.5,7.84754683803257,0.196236128096295));
#45150=CARTESIAN_POINT('',(1.35,7.99750013020562,0.199979167317699));
#45151=CARTESIAN_POINT('Ctrl Pts',(1.5,7.84754700261752,0.196229557926939));
#45152=CARTESIAN_POINT('Ctrl Pts',(1.45,7.89753132265494,0.197481659599516));
#45153=CARTESIAN_POINT('Ctrl Pts',(1.4,7.94751564245708,0.198733760838668));
#45154=CARTESIAN_POINT('Ctrl Pts',(1.35,7.9974999624945,0.199985862511245));
#45155=CARTESIAN_POINT('Ctrl Pts',(1.35,7.99750013020562,0.199979167317675));
#45156=CARTESIAN_POINT('Ctrl Pts',(1.34999999999993,7.96045345605724,1.67894428791948));
#45157=CARTESIAN_POINT('Ctrl Pts',(1.35000000000002,7.04769027505713,4.60637541289036));
#45158=CARTESIAN_POINT('Ctrl Pts',(1.34999999999998,3.56960738603504,7.62990378413704));
#45159=CARTESIAN_POINT('Ctrl Pts',(1.35000000000001,0.396409491081574,8.14001251989417));
#45160=CARTESIAN_POINT('Ctrl Pts',(1.35,-3.09406975939854,7.6429377715107));
#45161=CARTESIAN_POINT('Ctrl Pts',(1.35,-6.73863821231263,5.52525552672008));
#45162=CARTESIAN_POINT('Ctrl Pts',(1.35,-8.71268910481122,-0.247825284025847));
#45163=CARTESIAN_POINT('Ctrl Pts',(1.35,-6.34174153565703,-6.08130282678338));
#45164=CARTESIAN_POINT('Ctrl Pts',(1.35,-1.06987251858278,-8.53833317296371));
#45165=CARTESIAN_POINT('Ctrl Pts',(1.35,3.9038900172736,-7.41877209752381));
#45166=CARTESIAN_POINT('Ctrl Pts',(1.35,7.12113054186457,-4.42732247958672));
#45167=CARTESIAN_POINT('Ctrl Pts',(1.35,7.96199706750886,-1.61732074123609));
#45168=CARTESIAN_POINT('Ctrl Pts',(1.35,7.99750013020562,-0.199979167317696));
#45169=CARTESIAN_POINT('Origin',(0.,7.99750013020562,-0.199979167317696));
#45170=CARTESIAN_POINT('',(0.15,7.99750004634874,-0.199982514912803));
#45171=CARTESIAN_POINT('',(0.,7.99750013020562,-0.199979167317696));
#45172=CARTESIAN_POINT('',(0.,7.84754700261759,-0.196229557926829));
#45173=CARTESIAN_POINT('Ctrl Pts',(0.,7.84754700261759,-0.196229557926836));
#45174=CARTESIAN_POINT('Ctrl Pts',(0.05,7.89753132257661,-0.197481659453884));
#45175=CARTESIAN_POINT('Ctrl Pts',(0.1,7.94751564253563,-0.198733760980932));
#45176=CARTESIAN_POINT('Ctrl Pts',(0.15,7.99749996249466,-0.19998586250798));
#45177=CARTESIAN_POINT('',(0.,7.04779698988764,-0.17623164120232));
#45178=CARTESIAN_POINT('',(0.,7.99750013020562,-0.199979167317696));
#45179=CARTESIAN_POINT('',(0.15,6.89784386230235,-0.172482031811513));
#45180=CARTESIAN_POINT('Ctrl Pts',(0.15,6.89784386230235,-0.172482031811513));
#45181=CARTESIAN_POINT('Ctrl Pts',(0.125000000000001,6.92283605023323,-0.173106966709981));
#45182=CARTESIAN_POINT('Ctrl Pts',(0.100000000000001,6.94782823816411,-0.173731901608448));
#45183=CARTESIAN_POINT('Ctrl Pts',(0.0500000000000009,6.99781261402587,
-0.174981771405384));
#45184=CARTESIAN_POINT('Ctrl Pts',(0.0250000000000005,7.02280480195676,
-0.175606706303851));
#45185=CARTESIAN_POINT('Ctrl Pts',(0.,7.04779698988764,-0.176231641202319));
#45186=CARTESIAN_POINT('',(1.35,6.89784386230235,-0.172482031811513));
#45187=CARTESIAN_POINT('',(0.,6.89784386230235,-0.172482031811513));
#45188=CARTESIAN_POINT('',(1.5,7.04779698988764,-0.176231641202319));
#45189=CARTESIAN_POINT('Ctrl Pts',(1.5,7.04779698988764,-0.17623164120232));
#45190=CARTESIAN_POINT('Ctrl Pts',(1.475,7.02280480195676,-0.175606706303852));
#45191=CARTESIAN_POINT('Ctrl Pts',(1.45,6.99781261402588,-0.174981771405384));
#45192=CARTESIAN_POINT('Ctrl Pts',(1.4,6.94782823816411,-0.173731901608449));
#45193=CARTESIAN_POINT('Ctrl Pts',(1.375,6.92283605023323,-0.173106966709981));
#45194=CARTESIAN_POINT('Ctrl Pts',(1.35,6.89784386230235,-0.172482031811513));
#45195=CARTESIAN_POINT('',(1.5,7.99750013020562,-0.199979167317696));
#45196=CARTESIAN_POINT('Ctrl Pts',(0.,7.99750013020562,0.199979167317699));
#45197=CARTESIAN_POINT('Ctrl Pts',(1.5,7.99750013020562,0.199979167317699));
#45198=CARTESIAN_POINT('Ctrl Pts',(0.,7.99680550506533,0.227709763328977));
#45199=CARTESIAN_POINT('Ctrl Pts',(1.5,7.99680550506533,0.227709763328977));
#45200=CARTESIAN_POINT('Ctrl Pts',(0.,7.99517719352766,0.283151319739461));
#45201=CARTESIAN_POINT('Ctrl Pts',(1.5,7.99517719352766,0.283151319739461));
#45202=CARTESIAN_POINT('Ctrl Pts',(0.,7.99201754244988,0.366254747518976));
#45203=CARTESIAN_POINT('Ctrl Pts',(1.5,7.99201754244988,0.366254747518976));
#45204=CARTESIAN_POINT('Ctrl Pts',(0.,7.98637028878955,0.476941502739911));
#45205=CARTESIAN_POINT('Ctrl Pts',(1.5,7.98637028878955,0.476941502739911));
#45206=CARTESIAN_POINT('Ctrl Pts',(0.,7.97692078469299,0.615101120651634));
#45207=CARTESIAN_POINT('Ctrl Pts',(1.5,7.97692078469299,0.615101120651634));
#45208=CARTESIAN_POINT('Ctrl Pts',(0.,7.96508164046245,0.75305452456902));
#45209=CARTESIAN_POINT('Ctrl Pts',(1.5,7.96508164046245,0.75305452456902));
#45210=CARTESIAN_POINT('Ctrl Pts',(0.,7.95085458504529,0.890786949553286));
#45211=CARTESIAN_POINT('Ctrl Pts',(1.5,7.95085458504529,0.890786949553286));
#45212=CARTESIAN_POINT('Ctrl Pts',(0.,7.93424262024774,1.02827379662482));
#45213=CARTESIAN_POINT('Ctrl Pts',(1.5,7.93424262024774,1.02827379662482));
#45214=CARTESIAN_POINT('Ctrl Pts',(0.,7.91525036159975,1.16547817540896));
#45215=CARTESIAN_POINT('Ctrl Pts',(1.5,7.91525036159975,1.16547817540896));
#45216=CARTESIAN_POINT('Ctrl Pts',(0.,7.89388377445281,1.302354563183));
#45217=CARTESIAN_POINT('Ctrl Pts',(1.5,7.89388377445281,1.302354563183));
#45218=CARTESIAN_POINT('Ctrl Pts',(0.,7.8701499101466,1.43885246359671));
#45219=CARTESIAN_POINT('Ctrl Pts',(1.5,7.8701499101466,1.43885246359671));
#45220=CARTESIAN_POINT('Ctrl Pts',(0.,7.84405664223428,1.57492006520944));
#45221=CARTESIAN_POINT('Ctrl Pts',(1.5,7.84405664223428,1.57492006520944));
#45222=CARTESIAN_POINT('Ctrl Pts',(0.,7.81561240275637,1.71050789997905));
#45223=CARTESIAN_POINT('Ctrl Pts',(1.5,7.81561240275637,1.71050789997905));
#45224=CARTESIAN_POINT('Ctrl Pts',(0.,7.78482591855295,1.84557250184531));
#45225=CARTESIAN_POINT('Ctrl Pts',(1.5,7.78482591855295,1.84557250184531));
#45226=CARTESIAN_POINT('Ctrl Pts',(0.,7.7517063259076,1.98007473729323));
#45227=CARTESIAN_POINT('Ctrl Pts',(1.5,7.7517063259076,1.98007473729323));
#45228=CARTESIAN_POINT('Ctrl Pts',(0.,7.71626328522376,2.11397813608642));
#45229=CARTESIAN_POINT('Ctrl Pts',(1.5,7.71626328522376,2.11397813608642));
#45230=CARTESIAN_POINT('Ctrl Pts',(0.,7.67850709573848,2.24724722210367));
#45231=CARTESIAN_POINT('Ctrl Pts',(1.5,7.67850709573848,2.24724722210367));
#45232=CARTESIAN_POINT('Ctrl Pts',(0.,7.63844881027727,2.37984584421849));
#45233=CARTESIAN_POINT('Ctrl Pts',(1.5,7.63844881027727,2.37984584421849));
#45234=CARTESIAN_POINT('Ctrl Pts',(0.,7.59610035005487,2.51173550715644));
#45235=CARTESIAN_POINT('Ctrl Pts',(1.5,7.59610035005487,2.51173550715644));
#45236=CARTESIAN_POINT('Ctrl Pts',(0.,7.55147444968317,2.64287611205357));
#45237=CARTESIAN_POINT('Ctrl Pts',(1.5,7.55147444968317,2.64287611205357));
#45238=CARTESIAN_POINT('Ctrl Pts',(0.,7.50458460222712,2.77322669695875));
#45239=CARTESIAN_POINT('Ctrl Pts',(1.5,7.50458460222712,2.77322669695875));
#45240=CARTESIAN_POINT('Ctrl Pts',(0.,7.4554450043059,2.90274617730927));
#45241=CARTESIAN_POINT('Ctrl Pts',(1.5,7.4554450043059,2.90274617730927));
#45242=CARTESIAN_POINT('Ctrl Pts',(0.,7.40407050123783,3.03139408640743));
#45243=CARTESIAN_POINT('Ctrl Pts',(1.5,7.40407050123783,3.03139408640743));
#45244=CARTESIAN_POINT('Ctrl Pts',(0.,7.3504765322259,3.15913131592731));
#45245=CARTESIAN_POINT('Ctrl Pts',(1.5,7.3504765322259,3.15913131592731));
#45246=CARTESIAN_POINT('Ctrl Pts',(0.,7.29467914718133,3.28591981327769));
#45247=CARTESIAN_POINT('Ctrl Pts',(1.5,7.29467914718133,3.28591981327769));
#45248=CARTESIAN_POINT('Ctrl Pts',(0.,7.23669502358639,3.41172227901232));
#45249=CARTESIAN_POINT('Ctrl Pts',(1.5,7.23669502358639,3.41172227901232));
#45250=CARTESIAN_POINT('Ctrl Pts',(0.,7.17654148339747,3.53650186427506));
#45251=CARTESIAN_POINT('Ctrl Pts',(1.5,7.17654148339747,3.53650186427506));
#45252=CARTESIAN_POINT('Ctrl Pts',(0.,7.11423650998858,3.66022186826995));
#45253=CARTESIAN_POINT('Ctrl Pts',(1.5,7.11423650998858,3.66022186826995));
#45254=CARTESIAN_POINT('Ctrl Pts',(0.,7.0497987651361,3.78284543574385));
#45255=CARTESIAN_POINT('Ctrl Pts',(1.5,7.0497987651361,3.78284543574385));
#45256=CARTESIAN_POINT('Ctrl Pts',(0.,6.98324757351643,3.90433570307324));
#45257=CARTESIAN_POINT('Ctrl Pts',(1.5,6.98324757351643,3.90433570307324));
#45258=CARTESIAN_POINT('Ctrl Pts',(0.,6.91460290724501,4.02465594435869));
#45259=CARTESIAN_POINT('Ctrl Pts',(1.5,6.91460290724501,4.02465594435869));
#45260=CARTESIAN_POINT('Ctrl Pts',(0.,6.84388537045522,4.14376971753289));
#45261=CARTESIAN_POINT('Ctrl Pts',(1.5,6.84388537045522,4.14376971753289));
#45262=CARTESIAN_POINT('Ctrl Pts',(0.,6.7711161839166,4.26164101048806));
#45263=CARTESIAN_POINT('Ctrl Pts',(1.5,6.7711161839166,4.26164101048806));
#45264=CARTESIAN_POINT('Ctrl Pts',(0.,6.69631716969182,4.3782343872287));
#45265=CARTESIAN_POINT('Ctrl Pts',(1.5,6.69631716969182,4.3782343872287));
#45266=CARTESIAN_POINT('Ctrl Pts',(0.,6.61951074822057,4.49351493997149));
#45267=CARTESIAN_POINT('Ctrl Pts',(1.5,6.61951074822057,4.49351493997149));
#45268=CARTESIAN_POINT('Ctrl Pts',(0.,6.54071993544069,4.60744824127455));
#45269=CARTESIAN_POINT('Ctrl Pts',(1.5,6.54071993544069,4.60744824127455));
#45270=CARTESIAN_POINT('Ctrl Pts',(0.,6.45996833994703,4.72000029619479));
#45271=CARTESIAN_POINT('Ctrl Pts',(1.5,6.45996833994703,4.72000029619479));
#45272=CARTESIAN_POINT('Ctrl Pts',(0.,6.37728016018709,4.83113749447132));
#45273=CARTESIAN_POINT('Ctrl Pts',(1.5,6.37728016018709,4.83113749447132));
#45274=CARTESIAN_POINT('Ctrl Pts',(0.,6.29268018169369,4.94082656273376));
#45275=CARTESIAN_POINT('Ctrl Pts',(1.5,6.29268018169369,4.94082656273376));
#45276=CARTESIAN_POINT('Ctrl Pts',(0.,6.20619376748869,5.04903459924095));
#45277=CARTESIAN_POINT('Ctrl Pts',(1.5,6.20619376748869,5.04903459924095));
#45278=CARTESIAN_POINT('Ctrl Pts',(0.,6.11784684852259,5.15572910864443));
#45279=CARTESIAN_POINT('Ctrl Pts',(1.5,6.11784684852259,5.15572910864443));
#45280=CARTESIAN_POINT('Ctrl Pts',(0.,6.02766591414962,5.26087803677814));
#45281=CARTESIAN_POINT('Ctrl Pts',(1.5,6.02766591414962,5.26087803677814));
#45282=CARTESIAN_POINT('Ctrl Pts',(0.,5.93567800263764,5.36444980547617));
#45283=CARTESIAN_POINT('Ctrl Pts',(1.5,5.93567800263764,5.36444980547617));
#45284=CARTESIAN_POINT('Ctrl Pts',(0.,5.84191069171256,5.46641334741981));
#45285=CARTESIAN_POINT('Ctrl Pts',(1.5,5.84191069171256,5.46641334741981));
#45286=CARTESIAN_POINT('Ctrl Pts',(0.,5.7463920906582,5.56673810430368));
#45287=CARTESIAN_POINT('Ctrl Pts',(1.5,5.7463920906582,5.56673810430368));
#45288=CARTESIAN_POINT('Ctrl Pts',(0.,5.64915083244991,5.66539402503307));
#45289=CARTESIAN_POINT('Ctrl Pts',(1.5,5.64915083244991,5.66539402503307));
#45290=CARTESIAN_POINT('Ctrl Pts',(0.,5.55021606592043,5.7623515639526));
#45291=CARTESIAN_POINT('Ctrl Pts',(1.5,5.55021606592043,5.7623515639526));
#45292=CARTESIAN_POINT('Ctrl Pts',(0.,5.4496174479585,5.85758167910642));
#45293=CARTESIAN_POINT('Ctrl Pts',(1.5,5.4496174479585,5.85758167910642));
#45294=CARTESIAN_POINT('Ctrl Pts',(0.,5.34738513573868,5.95105583052966));
#45295=CARTESIAN_POINT('Ctrl Pts',(1.5,5.34738513573868,5.95105583052966));
#45296=CARTESIAN_POINT('Ctrl Pts',(0.,5.24354977700161,6.04274599307213));
#45297=CARTESIAN_POINT('Ctrl Pts',(1.5,5.24354977700161,6.04274599307213));
#45298=CARTESIAN_POINT('Ctrl Pts',(0.,5.13814250036456,6.13262466925426));
#45299=CARTESIAN_POINT('Ctrl Pts',(1.5,5.13814250036456,6.13262466925426));
#45300=CARTESIAN_POINT('Ctrl Pts',(0.,5.03119490566216,6.22066490215623));
#45301=CARTESIAN_POINT('Ctrl Pts',(1.5,5.03119490566216,6.22066490215623));
#45302=CARTESIAN_POINT('Ctrl Pts',(0.,4.92273905431653,6.30684028834105));
#45303=CARTESIAN_POINT('Ctrl Pts',(1.5,4.92273905431653,6.30684028834105));
#45304=CARTESIAN_POINT('Ctrl Pts',(0.,4.81280745973631,6.39112499081213));
#45305=CARTESIAN_POINT('Ctrl Pts',(1.5,4.81280745973631,6.39112499081213));
#45306=CARTESIAN_POINT('Ctrl Pts',(0.,4.70143307738903,6.47349374434624));
#45307=CARTESIAN_POINT('Ctrl Pts',(1.5,4.70143307738903,6.47349374434624));
#45308=CARTESIAN_POINT('Ctrl Pts',(0.,4.58864929490092,6.55392186086201));
#45309=CARTESIAN_POINT('Ctrl Pts',(1.5,4.58864929490092,6.55392186086201));
#45310=CARTESIAN_POINT('Ctrl Pts',(0.,4.47448992218395,6.6323852348246));
#45311=CARTESIAN_POINT('Ctrl Pts',(1.5,4.47448992218395,6.6323852348246));
#45312=CARTESIAN_POINT('Ctrl Pts',(0.,4.35898918158915,6.70886034868665));
#45313=CARTESIAN_POINT('Ctrl Pts',(1.5,4.35898918158915,6.70886034868665));
#45314=CARTESIAN_POINT('Ctrl Pts',(0.,4.24218169808576,6.78332427836609));
#45315=CARTESIAN_POINT('Ctrl Pts',(1.5,4.24218169808576,6.78332427836609));
#45316=CARTESIAN_POINT('Ctrl Pts',(0.,4.12410248853737,6.85575470054339));
#45317=CARTESIAN_POINT('Ctrl Pts',(1.5,4.12410248853737,6.85575470054339));
#45318=CARTESIAN_POINT('Ctrl Pts',(0.,4.00478695100247,6.92612989999665));
#45319=CARTESIAN_POINT('Ctrl Pts',(1.5,4.00478695100247,6.92612989999665));
#45320=CARTESIAN_POINT('Ctrl Pts',(0.,3.8842708540588,6.99442877697431));
#45321=CARTESIAN_POINT('Ctrl Pts',(1.5,3.8842708540588,6.99442877697431));
#45322=CARTESIAN_POINT('Ctrl Pts',(0.,3.76259032615098,7.06063085460664));
#45323=CARTESIAN_POINT('Ctrl Pts',(1.5,3.76259032615098,7.06063085460664));
#45324=CARTESIAN_POINT('Ctrl Pts',(0.,3.6397818449606,7.12471628635595));
#45325=CARTESIAN_POINT('Ctrl Pts',(1.5,3.6397818449606,7.12471628635595));
#45326=CARTESIAN_POINT('Ctrl Pts',(0.,3.51588222625163,7.18666586113527));
#45327=CARTESIAN_POINT('Ctrl Pts',(1.5,3.51588222625163,7.18666586113527));
#45328=CARTESIAN_POINT('Ctrl Pts',(0.,3.39092861273723,7.24646100846688));
#45329=CARTESIAN_POINT('Ctrl Pts',(1.5,3.39092861273723,7.24646100846688));
#45330=CARTESIAN_POINT('Ctrl Pts',(0.,3.26495846296687,7.30408380368079));
#45331=CARTESIAN_POINT('Ctrl Pts',(1.5,3.26495846296687,7.30408380368079));
#45332=CARTESIAN_POINT('Ctrl Pts',(0.,3.13800954023332,7.35951697315365));
#45333=CARTESIAN_POINT('Ctrl Pts',(1.5,3.13800954023332,7.35951697315365));
#45334=CARTESIAN_POINT('Ctrl Pts',(0.,3.01011990149853,7.41274389958825));
#45335=CARTESIAN_POINT('Ctrl Pts',(1.5,3.01011990149853,7.41274389958825));
#45336=CARTESIAN_POINT('Ctrl Pts',(0.,2.88132788576944,7.46374862667568));
#45337=CARTESIAN_POINT('Ctrl Pts',(1.5,2.88132788576944,7.46374862667568));
#45338=CARTESIAN_POINT('Ctrl Pts',(0.,2.75167210249136,7.51251586379888));
#45339=CARTESIAN_POINT('Ctrl Pts',(1.5,2.75167210249136,7.51251586379888));
#45340=CARTESIAN_POINT('Ctrl Pts',(0.,2.62119141995823,7.55903099077765));
#45341=CARTESIAN_POINT('Ctrl Pts',(1.5,2.62119141995823,7.55903099077765));
#45342=CARTESIAN_POINT('Ctrl Pts',(0.,2.48992495373916,7.60328006265563));
#45343=CARTESIAN_POINT('Ctrl Pts',(1.5,2.48992495373916,7.60328006265563));
#45344=CARTESIAN_POINT('Ctrl Pts',(0.,2.35791205512022,7.64524981452938));
#45345=CARTESIAN_POINT('Ctrl Pts',(1.5,2.35791205512022,7.64524981452938));
#45346=CARTESIAN_POINT('Ctrl Pts',(0.,2.22519229915043,7.68492766496107));
#45347=CARTESIAN_POINT('Ctrl Pts',(1.5,2.22519229915043,7.68492766496107));
#45348=CARTESIAN_POINT('Ctrl Pts',(0.,2.09180547270157,7.72230171943385));
#45349=CARTESIAN_POINT('Ctrl Pts',(1.5,2.09180547270157,7.72230171943385));
#45350=CARTESIAN_POINT('Ctrl Pts',(0.,1.95779156254141,7.75736077385028));
#45351=CARTESIAN_POINT('Ctrl Pts',(1.5,1.95779156254141,7.75736077385028));
#45352=CARTESIAN_POINT('Ctrl Pts',(0.,1.82319074341923,7.79009431807383));
#45353=CARTESIAN_POINT('Ctrl Pts',(1.5,1.82319074341923,7.79009431807383));
#45354=CARTESIAN_POINT('Ctrl Pts',(0.,1.68804336616321,7.82049253951376));
#45355=CARTESIAN_POINT('Ctrl Pts',(1.5,1.68804336616321,7.82049253951376));
#45356=CARTESIAN_POINT('Ctrl Pts',(0.,1.55238994546332,7.84854632558908));
#45357=CARTESIAN_POINT('Ctrl Pts',(1.5,1.55238994546332,7.84854632558908));
#45358=CARTESIAN_POINT('Ctrl Pts',(0.,1.41627114766429,7.8742472662363));
#45359=CARTESIAN_POINT('Ctrl Pts',(1.5,1.41627114766429,7.8742472662363));
#45360=CARTESIAN_POINT('Ctrl Pts',(0.,1.27972777856816,7.89758765646114));
#45361=CARTESIAN_POINT('Ctrl Pts',(1.5,1.27972777856816,7.89758765646114));
#45362=CARTESIAN_POINT('Ctrl Pts',(0.,1.14280077124554,7.9185604989343));
#45363=CARTESIAN_POINT('Ctrl Pts',(1.5,1.14280077124554,7.9185604989343));
#45364=CARTESIAN_POINT('Ctrl Pts',(0.,1.00553117385475,7.93715950663143));
#45365=CARTESIAN_POINT('Ctrl Pts',(1.5,1.00553117385475,7.93715950663143));
#45366=CARTESIAN_POINT('Ctrl Pts',(0.,0.867960137262833,7.95337910418951));
#45367=CARTESIAN_POINT('Ctrl Pts',(1.5,0.867960137262833,7.95337910418951));
#45368=CARTESIAN_POINT('Ctrl Pts',(0.,0.730128902672967,7.96721442930753));
#45369=CARTESIAN_POINT('Ctrl Pts',(1.5,0.730128902672967,7.96721442930753));
#45370=CARTESIAN_POINT('Ctrl Pts',(0.,0.5920787892575,7.97866133419203));
#45371=CARTESIAN_POINT('Ctrl Pts',(1.5,0.5920787892575,7.97866133419203));
#45372=CARTESIAN_POINT('Ctrl Pts',(0.,0.453851181796014,7.987716387047));
#45373=CARTESIAN_POINT('Ctrl Pts',(1.5,0.453851181796014,7.987716387047));
#45374=CARTESIAN_POINT('Ctrl Pts',(0.,0.315487518317418,7.99437687360893));
#45375=CARTESIAN_POINT('Ctrl Pts',(1.5,0.315487518317418,7.99437687360893));
#45376=CARTESIAN_POINT('Ctrl Pts',(0.,0.177029277647647,7.99864079744603));
#45377=CARTESIAN_POINT('Ctrl Pts',(1.5,0.177029277647647,7.99864079744603));
#45378=CARTESIAN_POINT('Ctrl Pts',(0.,0.0385179669598796,8.00050688030184));
#45379=CARTESIAN_POINT('Ctrl Pts',(1.5,0.0385179669598796,8.00050688030184));
#45380=CARTESIAN_POINT('Ctrl Pts',(0.,-0.100004890673484,7.99997456248424));
#45381=CARTESIAN_POINT('Ctrl Pts',(1.5,-0.100004890673484,7.99997456248424));
#45382=CARTESIAN_POINT('Ctrl Pts',(0.,-0.238497768727719,7.99704400329904));
#45383=CARTESIAN_POINT('Ctrl Pts',(1.5,-0.238497768727719,7.99704400329904));
#45384=CARTESIAN_POINT('Ctrl Pts',(0.,-0.376919149672484,7.99171608152879));
#45385=CARTESIAN_POINT('Ctrl Pts',(1.5,-0.376919149672484,7.99171608152879));
#45386=CARTESIAN_POINT('Ctrl Pts',(0.,-0.51522753740225,7.98399239464616));
#45387=CARTESIAN_POINT('Ctrl Pts',(1.5,-0.51522753740225,7.98399239464616));
#45388=CARTESIAN_POINT('Ctrl Pts',(0.,-0.653381469668191,7.97387525807239));
#45389=CARTESIAN_POINT('Ctrl Pts',(1.5,-0.653381469668191,7.97387525807239));
#45390=CARTESIAN_POINT('Ctrl Pts',(0.,-0.79133953051216,7.96136770448041));
#45391=CARTESIAN_POINT('Ctrl Pts',(1.5,-0.79133953051216,7.96136770448041));
#45392=CARTESIAN_POINT('Ctrl Pts',(0.,-0.929060362703415,7.9464734831431));
#45393=CARTESIAN_POINT('Ctrl Pts',(1.5,-0.929060362703415,7.9464734831431));
#45394=CARTESIAN_POINT('Ctrl Pts',(0.,-1.06650268017919,7.92919705932597));
#45395=CARTESIAN_POINT('Ctrl Pts',(1.5,-1.06650268017919,7.92919705932597));
#45396=CARTESIAN_POINT('Ctrl Pts',(0.,-1.20362528036102,7.90954361243223));
#45397=CARTESIAN_POINT('Ctrl Pts',(1.5,-1.20362528036102,7.90954361243223));
#45398=CARTESIAN_POINT('Ctrl Pts',(0.,-1.34038705647638,7.88751903419278));
#45399=CARTESIAN_POINT('Ctrl Pts',(1.5,-1.34038705647638,7.88751903419278));
#45400=CARTESIAN_POINT('Ctrl Pts',(0.,-1.47674700988613,7.86312992690012));
#45401=CARTESIAN_POINT('Ctrl Pts',(1.5,-1.47674700988613,7.86312992690012));
#45402=CARTESIAN_POINT('Ctrl Pts',(0.,-1.61266426241897,7.83638360168696));
#45403=CARTESIAN_POINT('Ctrl Pts',(1.5,-1.61266426241897,7.83638360168696));
#45404=CARTESIAN_POINT('Ctrl Pts',(0.,-1.74809806871318,7.80728807684891));
#45405=CARTESIAN_POINT('Ctrl Pts',(1.5,-1.74809806871318,7.80728807684891));
#45406=CARTESIAN_POINT('Ctrl Pts',(0.,-1.88300782832634,7.77585207492992));
#45407=CARTESIAN_POINT('Ctrl Pts',(1.5,-1.88300782832634,7.77585207492992));
#45408=CARTESIAN_POINT('Ctrl Pts',(0.,-2.01735309785401,7.74208501985214));
#45409=CARTESIAN_POINT('Ctrl Pts',(1.5,-2.01735309785401,7.74208501985214));
#45410=CARTESIAN_POINT('Ctrl Pts',(0.,-2.15109360305827,7.70599703408921));
#45411=CARTESIAN_POINT('Ctrl Pts',(1.5,-2.15109360305827,7.70599703408921));
#45412=CARTESIAN_POINT('Ctrl Pts',(0.,-2.28418925100688,7.66759893588344));
#45413=CARTESIAN_POINT('Ctrl Pts',(1.5,-2.28418925100688,7.66759893588344));
#45414=CARTESIAN_POINT('Ctrl Pts',(0.,-2.41660014222365,7.62690223650643));
#45415=CARTESIAN_POINT('Ctrl Pts',(1.5,-2.41660014222365,7.62690223650643));
#45416=CARTESIAN_POINT('Ctrl Pts',(0.,-2.54828658250082,7.58391913630904));
#45417=CARTESIAN_POINT('Ctrl Pts',(1.5,-2.54828658250082,7.58391913630904));
#45418=CARTESIAN_POINT('Ctrl Pts',(0.,-2.67920909472433,7.53866252081464));
#45419=CARTESIAN_POINT('Ctrl Pts',(1.5,-2.67920909472433,7.53866252081464));
#45420=CARTESIAN_POINT('Ctrl Pts',(0.,-2.80932843071254,7.49114595685495));
#45421=CARTESIAN_POINT('Ctrl Pts',(1.5,-2.80932843071254,7.49114595685495));
#45422=CARTESIAN_POINT('Ctrl Pts',(0.,-2.9386055830693,7.44138368874851));
#45423=CARTESIAN_POINT('Ctrl Pts',(1.5,-2.9386055830693,7.44138368874851));
#45424=CARTESIAN_POINT('Ctrl Pts',(0.,-3.06700179705218,7.38939063452162));
#45425=CARTESIAN_POINT('Ctrl Pts',(1.5,-3.06700179705218,7.38939063452162));
#45426=CARTESIAN_POINT('Ctrl Pts',(0.,-3.19447858199903,7.33518238095163));
#45427=CARTESIAN_POINT('Ctrl Pts',(1.5,-3.19447858199903,7.33518238095163));
#45428=CARTESIAN_POINT('Ctrl Pts',(0.,-3.32099772277123,7.27877517865203));
#45429=CARTESIAN_POINT('Ctrl Pts',(1.5,-3.32099772277123,7.27877517865203));
#45430=CARTESIAN_POINT('Ctrl Pts',(0.,-3.44652129121381,7.22018593719872));
#45431=CARTESIAN_POINT('Ctrl Pts',(1.5,-3.44652129121381,7.22018593719872));
#45432=CARTESIAN_POINT('Ctrl Pts',(0.,-3.57101165763383,7.15943222029806));
#45433=CARTESIAN_POINT('Ctrl Pts',(1.5,-3.57101165763383,7.15943222029806));
#45434=CARTESIAN_POINT('Ctrl Pts',(0.,-3.6944315022971,7.09653224099529));
#45435=CARTESIAN_POINT('Ctrl Pts',(1.5,-3.6944315022971,7.09653224099529));
#45436=CARTESIAN_POINT('Ctrl Pts',(0.,-3.8167438263836,7.03150485574848));
#45437=CARTESIAN_POINT('Ctrl Pts',(1.5,-3.8167438263836,7.03150485574848));
#45438=CARTESIAN_POINT('Ctrl Pts',(0.,-3.93791196296269,6.96436955854269));
#45439=CARTESIAN_POINT('Ctrl Pts',(1.5,-3.93791196296269,6.96436955854269));
#45440=CARTESIAN_POINT('Ctrl Pts',(0.,-4.05789958798918,6.89514647504389));
#45441=CARTESIAN_POINT('Ctrl Pts',(1.5,-4.05789958798918,6.89514647504389));
#45442=CARTESIAN_POINT('Ctrl Pts',(0.,-4.17667073132075,6.82385635679251));
#45443=CARTESIAN_POINT('Ctrl Pts',(1.5,-4.17667073132075,6.82385635679251));
#45444=CARTESIAN_POINT('Ctrl Pts',(0.,-4.29418978775755,6.75052057543597));
#45445=CARTESIAN_POINT('Ctrl Pts',(1.5,-4.29418978775755,6.75052057543597));
#45446=CARTESIAN_POINT('Ctrl Pts',(0.,-4.41042152744403,6.67516111587753));
#45447=CARTESIAN_POINT('Ctrl Pts',(1.5,-4.41042152744403,6.67516111587753));
#45448=CARTESIAN_POINT('Ctrl Pts',(0.,-4.52533110629424,6.59780056946357));
#45449=CARTESIAN_POINT('Ctrl Pts',(1.5,-4.52533110629424,6.59780056946357));
#45450=CARTESIAN_POINT('Ctrl Pts',(0.,-4.63888407644116,6.51846212720865));
#45451=CARTESIAN_POINT('Ctrl Pts',(1.5,-4.63888407644116,6.51846212720865));
#45452=CARTESIAN_POINT('Ctrl Pts',(0.,-4.75104639671082,6.43716957305794));
#45453=CARTESIAN_POINT('Ctrl Pts',(1.5,-4.75104639671082,6.43716957305794));
#45454=CARTESIAN_POINT('Ctrl Pts',(0.,-4.86178444312194,6.35394727718697));
#45455=CARTESIAN_POINT('Ctrl Pts',(1.5,-4.86178444312194,6.35394727718697));
#45456=CARTESIAN_POINT('Ctrl Pts',(0.,-4.97106501865637,6.26882018827667));
#45457=CARTESIAN_POINT('Ctrl Pts',(1.5,-4.97106501865637,6.26882018827667));
#45458=CARTESIAN_POINT('Ctrl Pts',(0.,-5.07885536305621,6.18181382582466));
#45459=CARTESIAN_POINT('Ctrl Pts',(1.5,-5.07885536305621,6.18181382582466));
#45460=CARTESIAN_POINT('Ctrl Pts',(0.,-5.18512316264831,6.09295427249219));
#45461=CARTESIAN_POINT('Ctrl Pts',(1.5,-5.18512316264831,6.09295427249219));
#45462=CARTESIAN_POINT('Ctrl Pts',(0.,-5.2898365601966,6.00226816648635));
#45463=CARTESIAN_POINT('Ctrl Pts',(1.5,-5.2898365601966,6.00226816648635));
#45464=CARTESIAN_POINT('Ctrl Pts',(0.,-5.392964164783,5.90978269397704));
#45465=CARTESIAN_POINT('Ctrl Pts',(1.5,-5.392964164783,5.90978269397704));
#45466=CARTESIAN_POINT('Ctrl Pts',(0.,-5.49447506087342,5.81552558055624));
#45467=CARTESIAN_POINT('Ctrl Pts',(1.5,-5.49447506087342,5.81552558055624));
#45468=CARTESIAN_POINT('Ctrl Pts',(0.,-5.59433881741343,5.71952508273097));
#45469=CARTESIAN_POINT('Ctrl Pts',(1.5,-5.59433881741343,5.71952508273097));
#45470=CARTESIAN_POINT('Ctrl Pts',(0.,-5.69252549695431,5.62180997944946));
#45471=CARTESIAN_POINT('Ctrl Pts',(1.5,-5.69252549695431,5.62180997944946));
#45472=CARTESIAN_POINT('Ctrl Pts',(0.,-5.78900566480983,5.52240956365993));
#45473=CARTESIAN_POINT('Ctrl Pts',(1.5,-5.78900566480983,5.52240956365993));
#45474=CARTESIAN_POINT('Ctrl Pts',(0.,-5.88375039824441,5.42135363390141));
#45475=CARTESIAN_POINT('Ctrl Pts',(1.5,-5.88375039824441,5.42135363390141));
#45476=CARTESIAN_POINT('Ctrl Pts',(0.,-5.97673129476659,5.31867248501124));
#45477=CARTESIAN_POINT('Ctrl Pts',(1.5,-5.97673129476659,5.31867248501124));
#45478=CARTESIAN_POINT('Ctrl Pts',(0.,-6.06792048045517,5.21439689886345));
#45479=CARTESIAN_POINT('Ctrl Pts',(1.5,-6.06792048045517,5.21439689886345));
#45480=CARTESIAN_POINT('Ctrl Pts',(0.,-6.15729061831829,5.10855813513777));
#45481=CARTESIAN_POINT('Ctrl Pts',(1.5,-6.15729061831829,5.10855813513777));
#45482=CARTESIAN_POINT('Ctrl Pts',(0.,-6.24481491668612,5.00118792211818));
#45483=CARTESIAN_POINT('Ctrl Pts',(1.5,-6.24481491668612,5.00118792211818));
#45484=CARTESIAN_POINT('Ctrl Pts',(0.,-6.33046713763756,4.89231844752085));
#45485=CARTESIAN_POINT('Ctrl Pts',(1.5,-6.33046713763756,4.89231844752085));
#45486=CARTESIAN_POINT('Ctrl Pts',(0.,-6.4142216044593,4.78198234851926));
#45487=CARTESIAN_POINT('Ctrl Pts',(1.5,-6.4142216044593,4.78198234851926));
#45488=CARTESIAN_POINT('Ctrl Pts',(0.,-6.49605320913994,4.67021270179733));
#45489=CARTESIAN_POINT('Ctrl Pts',(1.5,-6.49605320913994,4.67021270179733));
#45490=CARTESIAN_POINT('Ctrl Pts',(0.,-6.57593741989968,4.55704301363019));
#45491=CARTESIAN_POINT('Ctrl Pts',(1.5,-6.57593741989968,4.55704301363019));
#45492=CARTESIAN_POINT('Ctrl Pts',(0.,-6.65385028875591,4.44250720999153));
#45493=CARTESIAN_POINT('Ctrl Pts',(1.5,-6.65385028875591,4.44250720999153));
#45494=CARTESIAN_POINT('Ctrl Pts',(0.,-6.7297684591252,4.3266396266874));
#45495=CARTESIAN_POINT('Ctrl Pts',(1.5,-6.7297684591252,4.3266396266874));
#45496=CARTESIAN_POINT('Ctrl Pts',(0.,-6.80366917239198,4.20947499877372));
#45497=CARTESIAN_POINT('Ctrl Pts',(1.5,-6.80366917239198,4.20947499877372));
#45498=CARTESIAN_POINT('Ctrl Pts',(0.,-6.87553027451456,4.0910484499988));
#45499=CARTESIAN_POINT('Ctrl Pts',(1.5,-6.87553027451456,4.0910484499988));
#45500=CARTESIAN_POINT('Ctrl Pts',(0.,-6.94533022266887,3.97139548227007));
#45501=CARTESIAN_POINT('Ctrl Pts',(1.5,-6.94533022266887,3.97139548227007));
#45502=CARTESIAN_POINT('Ctrl Pts',(0.,-7.01304809193043,3.85055196514442));
#45503=CARTESIAN_POINT('Ctrl Pts',(1.5,-7.01304809193043,3.85055196514442));
#45504=CARTESIAN_POINT('Ctrl Pts',(0.,-7.07866358199495,3.72855412534148));
#45505=CARTESIAN_POINT('Ctrl Pts',(1.5,-7.07866358199495,3.72855412534148));
#45506=CARTESIAN_POINT('Ctrl Pts',(0.,-7.14215702280734,3.6054385356329));
#45507=CARTESIAN_POINT('Ctrl Pts',(1.5,-7.14215702280734,3.6054385356329));
#45508=CARTESIAN_POINT('Ctrl Pts',(0.,-7.2035093802301,3.48124210375322));
#45509=CARTESIAN_POINT('Ctrl Pts',(1.5,-7.2035093802301,3.48124210375322));
#45510=CARTESIAN_POINT('Ctrl Pts',(0.,-7.26270226175155,3.35600206133158));
#45511=CARTESIAN_POINT('Ctrl Pts',(1.5,-7.26270226175155,3.35600206133158));
#45512=CARTESIAN_POINT('Ctrl Pts',(0.,-7.31971792223396,3.22975595284375));
#45513=CARTESIAN_POINT('Ctrl Pts',(1.5,-7.31971792223396,3.22975595284375));
#45514=CARTESIAN_POINT('Ctrl Pts',(0.,-7.37453926970234,3.10254162458354));
#45515=CARTESIAN_POINT('Ctrl Pts',(1.5,-7.37453926970234,3.10254162458354));
#45516=CARTESIAN_POINT('Ctrl Pts',(0.,-7.42714986999163,2.97439721310696));
#45517=CARTESIAN_POINT('Ctrl Pts',(1.5,-7.42714986999163,2.97439721310696));
#45518=CARTESIAN_POINT('Ctrl Pts',(0.,-7.47753395143493,2.84536113369459));
#45519=CARTESIAN_POINT('Ctrl Pts',(1.5,-7.47753395143493,2.84536113369459));
#45520=CARTESIAN_POINT('Ctrl Pts',(0.,-7.52567640959341,2.7154720688311));
#45521=CARTESIAN_POINT('Ctrl Pts',(1.5,-7.52567640959341,2.7154720688311));
#45522=CARTESIAN_POINT('Ctrl Pts',(0.,-7.57156281202762,2.58476895670172));
#45523=CARTESIAN_POINT('Ctrl Pts',(1.5,-7.57156281202762,2.58476895670172));
#45524=CARTESIAN_POINT('Ctrl Pts',(0.,-7.61517940311102,2.45329097970451));
#45525=CARTESIAN_POINT('Ctrl Pts',(1.5,-7.61517940311102,2.45329097970451));
#45526=CARTESIAN_POINT('Ctrl Pts',(0.,-7.65651310766076,2.32107755253587));
#45527=CARTESIAN_POINT('Ctrl Pts',(1.5,-7.65651310766076,2.32107755253587));
#45528=CARTESIAN_POINT('Ctrl Pts',(0.,-7.69555153461076,2.18816831029056));
#45529=CARTESIAN_POINT('Ctrl Pts',(1.5,-7.69555153461076,2.18816831029056));
#45530=CARTESIAN_POINT('Ctrl Pts',(0.,-7.7322829807279,2.05460309657569));
#45531=CARTESIAN_POINT('Ctrl Pts',(1.5,-7.7322829807279,2.05460309657569));
#45532=CARTESIAN_POINT('Ctrl Pts',(0.,-7.76669643437085,1.92042195163751));
#45533=CARTESIAN_POINT('Ctrl Pts',(1.5,-7.76669643437085,1.92042195163751));
#45534=CARTESIAN_POINT('Ctrl Pts',(0.,-7.79878157929215,1.78566510050061));
#45535=CARTESIAN_POINT('Ctrl Pts',(1.5,-7.79878157929215,1.78566510050061));
#45536=CARTESIAN_POINT('Ctrl Pts',(0.,-7.82852879722494,1.65037294078415));
#45537=CARTESIAN_POINT('Ctrl Pts',(1.5,-7.82852879722494,1.65037294078415));
#45538=CARTESIAN_POINT('Ctrl Pts',(0.,-7.85592917051368,1.51458603052897));
#45539=CARTESIAN_POINT('Ctrl Pts',(1.5,-7.85592917051368,1.51458603052897));
#45540=CARTESIAN_POINT('Ctrl Pts',(0.,-7.88097448478828,1.37834507603462));
#45541=CARTESIAN_POINT('Ctrl Pts',(1.5,-7.88097448478828,1.37834507603462));
#45542=CARTESIAN_POINT('Ctrl Pts',(0.,-7.90365723168263,1.24169091970572));
#45543=CARTESIAN_POINT('Ctrl Pts',(1.5,-7.90365723168263,1.24169091970572));
#45544=CARTESIAN_POINT('Ctrl Pts',(0.,-7.92397061159682,1.10466452790671));
#45545=CARTESIAN_POINT('Ctrl Pts',(1.5,-7.92397061159682,1.10466452790671));
#45546=CARTESIAN_POINT('Ctrl Pts',(0.,-7.94190853522107,0.967306978600068));
#45547=CARTESIAN_POINT('Ctrl Pts',(1.5,-7.94190853522107,0.967306978600068));
#45548=CARTESIAN_POINT('Ctrl Pts',(0.,-7.95746562510374,0.829659448991489));
#45549=CARTESIAN_POINT('Ctrl Pts',(1.5,-7.95746562510374,0.829659448991489));
#45550=CARTESIAN_POINT('Ctrl Pts',(0.,-7.97063721726419,0.691763203181292));
#45551=CARTESIAN_POINT('Ctrl Pts',(1.5,-7.97063721726419,0.691763203181292));
#45552=CARTESIAN_POINT('Ctrl Pts',(0.,-7.98141936284981,0.553659579821253));
#45553=CARTESIAN_POINT('Ctrl Pts',(1.5,-7.98141936284981,0.553659579821253));
#45554=CARTESIAN_POINT('Ctrl Pts',(0.,-7.98980882983796,0.41538997977611));
#45555=CARTESIAN_POINT('Ctrl Pts',(1.5,-7.98980882983796,0.41538997977611));
#45556=CARTESIAN_POINT('Ctrl Pts',(0.,-7.9958031034851,0.276995853676294));
#45557=CARTESIAN_POINT('Ctrl Pts',(1.5,-7.9958031034851,0.276995853676294));
#45558=CARTESIAN_POINT('Ctrl Pts',(0.,-7.99940038682089,0.138518689473731));
#45559=CARTESIAN_POINT('Ctrl Pts',(1.5,-7.99940038682089,0.138518689473731));
#45560=CARTESIAN_POINT('Ctrl Pts',(0.,-8.00059960118697,7.404667157207E-14));
#45561=CARTESIAN_POINT('Ctrl Pts',(1.5,-8.00059960118697,7.404667157207E-14));
#45562=CARTESIAN_POINT('Ctrl Pts',(0.,-7.99940038682102,-0.138518689473581));
#45563=CARTESIAN_POINT('Ctrl Pts',(1.5,-7.99940038682102,-0.138518689473581));
#45564=CARTESIAN_POINT('Ctrl Pts',(0.,-7.99580310348534,-0.276995853676148));
#45565=CARTESIAN_POINT('Ctrl Pts',(1.5,-7.99580310348534,-0.276995853676148));
#45566=CARTESIAN_POINT('Ctrl Pts',(0.,-7.98980882983822,-0.415389979775981));
#45567=CARTESIAN_POINT('Ctrl Pts',(1.5,-7.98980882983822,-0.415389979775981));
#45568=CARTESIAN_POINT('Ctrl Pts',(0.,-7.98141936285002,-0.55365957982111));
#45569=CARTESIAN_POINT('Ctrl Pts',(1.5,-7.98141936285002,-0.55365957982111));
#45570=CARTESIAN_POINT('Ctrl Pts',(0.,-7.97063721726421,-0.691763203181143));
#45571=CARTESIAN_POINT('Ctrl Pts',(1.5,-7.97063721726421,-0.691763203181143));
#45572=CARTESIAN_POINT('Ctrl Pts',(0.,-7.95746562510355,-0.829659448991339));
#45573=CARTESIAN_POINT('Ctrl Pts',(1.5,-7.95746562510355,-0.829659448991339));
#45574=CARTESIAN_POINT('Ctrl Pts',(0.,-7.94190853522072,-0.96730697859992));
#45575=CARTESIAN_POINT('Ctrl Pts',(1.5,-7.94190853522072,-0.96730697859992));
#45576=CARTESIAN_POINT('Ctrl Pts',(0.,-7.92397061159648,-1.10466452790657));
#45577=CARTESIAN_POINT('Ctrl Pts',(1.5,-7.92397061159648,-1.10466452790657));
#45578=CARTESIAN_POINT('Ctrl Pts',(0.,-7.90365723168241,-1.24169091970559));
#45579=CARTESIAN_POINT('Ctrl Pts',(1.5,-7.90365723168241,-1.24169091970559));
#45580=CARTESIAN_POINT('Ctrl Pts',(0.,-7.88097448478831,-1.37834507603449));
#45581=CARTESIAN_POINT('Ctrl Pts',(1.5,-7.88097448478831,-1.37834507603449));
#45582=CARTESIAN_POINT('Ctrl Pts',(0.,-7.85592917051396,-1.5145860305288));
#45583=CARTESIAN_POINT('Ctrl Pts',(1.5,-7.85592917051396,-1.5145860305288));
#45584=CARTESIAN_POINT('Ctrl Pts',(0.,-7.82852879722539,-1.65037294078395));
#45585=CARTESIAN_POINT('Ctrl Pts',(1.5,-7.82852879722539,-1.65037294078395));
#45586=CARTESIAN_POINT('Ctrl Pts',(0.,-7.7987815792926,-1.78566510050039));
#45587=CARTESIAN_POINT('Ctrl Pts',(1.5,-7.7987815792926,-1.78566510050039));
#45588=CARTESIAN_POINT('Ctrl Pts',(0.,-7.76669643437116,-1.92042195163732));
#45589=CARTESIAN_POINT('Ctrl Pts',(1.5,-7.76669643437116,-1.92042195163732));
#45590=CARTESIAN_POINT('Ctrl Pts',(0.,-7.73228298072794,-2.05460309657555));
#45591=CARTESIAN_POINT('Ctrl Pts',(1.5,-7.73228298072794,-2.05460309657555));
#45592=CARTESIAN_POINT('Ctrl Pts',(0.,-7.69555153461053,-2.18816831029048));
#45593=CARTESIAN_POINT('Ctrl Pts',(1.5,-7.69555153461053,-2.18816831029048));
#45594=CARTESIAN_POINT('Ctrl Pts',(0.,-7.6565131076604,-2.32107755253582));
#45595=CARTESIAN_POINT('Ctrl Pts',(1.5,-7.6565131076604,-2.32107755253582));
#45596=CARTESIAN_POINT('Ctrl Pts',(0.,-7.61517940311072,-2.45329097970447));
#45597=CARTESIAN_POINT('Ctrl Pts',(1.5,-7.61517940311072,-2.45329097970447));
#45598=CARTESIAN_POINT('Ctrl Pts',(0.,-7.57156281202747,-2.58476895670164));
#45599=CARTESIAN_POINT('Ctrl Pts',(1.5,-7.57156281202747,-2.58476895670164));
#45600=CARTESIAN_POINT('Ctrl Pts',(0.,-7.52567640959347,-2.71547206883096));
#45601=CARTESIAN_POINT('Ctrl Pts',(1.5,-7.52567640959347,-2.71547206883096));
#45602=CARTESIAN_POINT('Ctrl Pts',(0.,-7.47753395143517,-2.8453611336944));
#45603=CARTESIAN_POINT('Ctrl Pts',(1.5,-7.47753395143517,-2.8453611336944));
#45604=CARTESIAN_POINT('Ctrl Pts',(0.,-7.42714986999194,-2.97439721310677));
#45605=CARTESIAN_POINT('Ctrl Pts',(1.5,-7.42714986999194,-2.97439721310677));
#45606=CARTESIAN_POINT('Ctrl Pts',(0.,-7.37453926970263,-3.10254162458336));
#45607=CARTESIAN_POINT('Ctrl Pts',(1.5,-7.37453926970263,-3.10254162458336));
#45608=CARTESIAN_POINT('Ctrl Pts',(0.,-7.31971792223413,-3.22975595284362));
#45609=CARTESIAN_POINT('Ctrl Pts',(1.5,-7.31971792223413,-3.22975595284362));
#45610=CARTESIAN_POINT('Ctrl Pts',(0.,-7.26270226175159,-3.35600206133147));
#45611=CARTESIAN_POINT('Ctrl Pts',(1.5,-7.26270226175159,-3.35600206133147));
#45612=CARTESIAN_POINT('Ctrl Pts',(0.,-7.20350938023008,-3.48124210375305));
#45613=CARTESIAN_POINT('Ctrl Pts',(1.5,-7.20350938023008,-3.48124210375305));
#45614=CARTESIAN_POINT('Ctrl Pts',(0.,-7.14215702280731,-3.60543853563268));
#45615=CARTESIAN_POINT('Ctrl Pts',(1.5,-7.14215702280731,-3.60543853563268));
#45616=CARTESIAN_POINT('Ctrl Pts',(0.,-7.07866358199493,-3.72855412534125));
#45617=CARTESIAN_POINT('Ctrl Pts',(1.5,-7.07866358199493,-3.72855412534125));
#45618=CARTESIAN_POINT('Ctrl Pts',(0.,-7.01304809193044,-3.85055196514423));
#45619=CARTESIAN_POINT('Ctrl Pts',(1.5,-7.01304809193044,-3.85055196514423));
#45620=CARTESIAN_POINT('Ctrl Pts',(0.,-6.94533022266893,-3.97139548226995));
#45621=CARTESIAN_POINT('Ctrl Pts',(1.5,-6.94533022266893,-3.97139548226995));
#45622=CARTESIAN_POINT('Ctrl Pts',(0.,-6.8755302745147,-4.09104844999872));
#45623=CARTESIAN_POINT('Ctrl Pts',(1.5,-6.8755302745147,-4.09104844999872));
#45624=CARTESIAN_POINT('Ctrl Pts',(0.,-6.80366917239217,-4.20947499877361));
#45625=CARTESIAN_POINT('Ctrl Pts',(1.5,-6.80366917239217,-4.20947499877361));
#45626=CARTESIAN_POINT('Ctrl Pts',(0.,-6.7297684591254,-4.32663962668727));
#45627=CARTESIAN_POINT('Ctrl Pts',(1.5,-6.7297684591254,-4.32663962668727));
#45628=CARTESIAN_POINT('Ctrl Pts',(0.,-6.65385028875609,-4.44250720999139));
#45629=CARTESIAN_POINT('Ctrl Pts',(1.5,-6.65385028875609,-4.44250720999139));
#45630=CARTESIAN_POINT('Ctrl Pts',(0.,-6.57593741989978,-4.55704301363008));
#45631=CARTESIAN_POINT('Ctrl Pts',(1.5,-6.57593741989978,-4.55704301363008));
#45632=CARTESIAN_POINT('Ctrl Pts',(0.,-6.49605320913988,-4.67021270179723));
#45633=CARTESIAN_POINT('Ctrl Pts',(1.5,-6.49605320913988,-4.67021270179723));
#45634=CARTESIAN_POINT('Ctrl Pts',(0.,-6.41422160445912,-4.78198234851915));
#45635=CARTESIAN_POINT('Ctrl Pts',(1.5,-6.41422160445912,-4.78198234851915));
#45636=CARTESIAN_POINT('Ctrl Pts',(0.,-6.33046713763739,-4.89231844752076));
#45637=CARTESIAN_POINT('Ctrl Pts',(1.5,-6.33046713763739,-4.89231844752076));
#45638=CARTESIAN_POINT('Ctrl Pts',(0.,-6.24481491668607,-5.00118792211809));
#45639=CARTESIAN_POINT('Ctrl Pts',(1.5,-6.24481491668607,-5.00118792211809));
#45640=CARTESIAN_POINT('Ctrl Pts',(0.,-6.15729061831839,-5.10855813513767));
#45641=CARTESIAN_POINT('Ctrl Pts',(1.5,-6.15729061831839,-5.10855813513767));
#45642=CARTESIAN_POINT('Ctrl Pts',(0.,-6.06792048045539,-5.21439689886329));
#45643=CARTESIAN_POINT('Ctrl Pts',(1.5,-6.06792048045539,-5.21439689886329));
#45644=CARTESIAN_POINT('Ctrl Pts',(0.,-5.97673129476691,-5.31867248501106));
#45645=CARTESIAN_POINT('Ctrl Pts',(1.5,-5.97673129476691,-5.31867248501106));
#45646=CARTESIAN_POINT('Ctrl Pts',(0.,-5.88375039824476,-5.42135363390127));
#45647=CARTESIAN_POINT('Ctrl Pts',(1.5,-5.88375039824476,-5.42135363390127));
#45648=CARTESIAN_POINT('Ctrl Pts',(0.,-5.78900566481012,-5.52240956365984));
#45649=CARTESIAN_POINT('Ctrl Pts',(1.5,-5.78900566481012,-5.52240956365984));
#45650=CARTESIAN_POINT('Ctrl Pts',(0.,-5.69252549695442,-5.62180997944938));
#45651=CARTESIAN_POINT('Ctrl Pts',(1.5,-5.69252549695442,-5.62180997944938));
#45652=CARTESIAN_POINT('Ctrl Pts',(0.,-5.59433881741333,-5.71952508273083));
#45653=CARTESIAN_POINT('Ctrl Pts',(1.5,-5.59433881741333,-5.71952508273083));
#45654=CARTESIAN_POINT('Ctrl Pts',(0.,-5.4944750608732,-5.81552558055602));
#45655=CARTESIAN_POINT('Ctrl Pts',(1.5,-5.4944750608732,-5.81552558055602));
#45656=CARTESIAN_POINT('Ctrl Pts',(0.,-5.39296416478281,-5.90978269397678));
#45657=CARTESIAN_POINT('Ctrl Pts',(1.5,-5.39296416478281,-5.90978269397678));
#45658=CARTESIAN_POINT('Ctrl Pts',(0.,-5.28983656019654,-6.00226816648613));
#45659=CARTESIAN_POINT('Ctrl Pts',(1.5,-5.28983656019654,-6.00226816648613));
#45660=CARTESIAN_POINT('Ctrl Pts',(0.,-5.18512316264843,-6.09295427249209));
#45661=CARTESIAN_POINT('Ctrl Pts',(1.5,-5.18512316264843,-6.09295427249209));
#45662=CARTESIAN_POINT('Ctrl Pts',(0.,-5.07885536305647,-6.18181382582471));
#45663=CARTESIAN_POINT('Ctrl Pts',(1.5,-5.07885536305647,-6.18181382582471));
#45664=CARTESIAN_POINT('Ctrl Pts',(0.,-4.9710650186567,-6.26882018827681));
#45665=CARTESIAN_POINT('Ctrl Pts',(1.5,-4.9710650186567,-6.26882018827681));
#45666=CARTESIAN_POINT('Ctrl Pts',(0.,-4.86178444312227,-6.3539472771871));
#45667=CARTESIAN_POINT('Ctrl Pts',(1.5,-4.86178444312227,-6.3539472771871));
#45668=CARTESIAN_POINT('Ctrl Pts',(0.,-4.75104639671106,-6.43716957305797));
#45669=CARTESIAN_POINT('Ctrl Pts',(1.5,-4.75104639671106,-6.43716957305797));
#45670=CARTESIAN_POINT('Ctrl Pts',(0.,-4.63888407644128,-6.51846212720856));
#45671=CARTESIAN_POINT('Ctrl Pts',(1.5,-4.63888407644128,-6.51846212720856));
#45672=CARTESIAN_POINT('Ctrl Pts',(0.,-4.52533110629424,-6.59780056946339));
#45673=CARTESIAN_POINT('Ctrl Pts',(1.5,-4.52533110629424,-6.59780056946339));
#45674=CARTESIAN_POINT('Ctrl Pts',(0.,-4.41042152744394,-6.67516111587727));
#45675=CARTESIAN_POINT('Ctrl Pts',(1.5,-4.41042152744394,-6.67516111587727));
#45676=CARTESIAN_POINT('Ctrl Pts',(0.,-4.29418978775745,-6.75052057543572));
#45677=CARTESIAN_POINT('Ctrl Pts',(1.5,-4.29418978775745,-6.75052057543572));
#45678=CARTESIAN_POINT('Ctrl Pts',(0.,-4.17667073132073,-6.82385635679236));
#45679=CARTESIAN_POINT('Ctrl Pts',(1.5,-4.17667073132073,-6.82385635679236));
#45680=CARTESIAN_POINT('Ctrl Pts',(0.,-4.0578995879893,-6.89514647504383));
#45681=CARTESIAN_POINT('Ctrl Pts',(1.5,-4.0578995879893,-6.89514647504383));
#45682=CARTESIAN_POINT('Ctrl Pts',(0.,-3.93791196296294,-6.96436955854269));
#45683=CARTESIAN_POINT('Ctrl Pts',(1.5,-3.93791196296294,-6.96436955854269));
#45684=CARTESIAN_POINT('Ctrl Pts',(0.,-3.81674382638391,-7.03150485574852));
#45685=CARTESIAN_POINT('Ctrl Pts',(1.5,-3.81674382638391,-7.03150485574852));
#45686=CARTESIAN_POINT('Ctrl Pts',(0.,-3.69443150229741,-7.09653224099531));
#45687=CARTESIAN_POINT('Ctrl Pts',(1.5,-3.69443150229741,-7.09653224099531));
#45688=CARTESIAN_POINT('Ctrl Pts',(0.,-3.57101165763407,-7.15943222029805));
#45689=CARTESIAN_POINT('Ctrl Pts',(1.5,-3.57101165763407,-7.15943222029805));
#45690=CARTESIAN_POINT('Ctrl Pts',(0.,-3.44652129121395,-7.22018593719866));
#45691=CARTESIAN_POINT('Ctrl Pts',(1.5,-3.44652129121395,-7.22018593719866));
#45692=CARTESIAN_POINT('Ctrl Pts',(0.,-3.32099772277122,-7.27877517865193));
#45693=CARTESIAN_POINT('Ctrl Pts',(1.5,-3.32099772277122,-7.27877517865193));
#45694=CARTESIAN_POINT('Ctrl Pts',(0.,-3.19447858199892,-7.33518238095157));
#45695=CARTESIAN_POINT('Ctrl Pts',(1.5,-3.19447858199892,-7.33518238095157));
#45696=CARTESIAN_POINT('Ctrl Pts',(0.,-3.06700179705205,-7.38939063452155));
#45697=CARTESIAN_POINT('Ctrl Pts',(1.5,-3.06700179705205,-7.38939063452155));
#45698=CARTESIAN_POINT('Ctrl Pts',(0.,-2.93860558306928,-7.44138368874846));
#45699=CARTESIAN_POINT('Ctrl Pts',(1.5,-2.93860558306928,-7.44138368874846));
#45700=CARTESIAN_POINT('Ctrl Pts',(0.,-2.80932843071268,-7.49114595685492));
#45701=CARTESIAN_POINT('Ctrl Pts',(1.5,-2.80932843071268,-7.49114595685492));
#45702=CARTESIAN_POINT('Ctrl Pts',(0.,-2.67920909472461,-7.53866252081456));
#45703=CARTESIAN_POINT('Ctrl Pts',(1.5,-2.67920909472461,-7.53866252081456));
#45704=CARTESIAN_POINT('Ctrl Pts',(0.,-2.54828658250114,-7.58391913630888));
#45705=CARTESIAN_POINT('Ctrl Pts',(1.5,-2.54828658250114,-7.58391913630888));
#45706=CARTESIAN_POINT('Ctrl Pts',(0.,-2.41660014222393,-7.62690223650621));
#45707=CARTESIAN_POINT('Ctrl Pts',(1.5,-2.41660014222393,-7.62690223650621));
#45708=CARTESIAN_POINT('Ctrl Pts',(0.,-2.28418925100709,-7.66759893588327));
#45709=CARTESIAN_POINT('Ctrl Pts',(1.5,-2.28418925100709,-7.66759893588327));
#45710=CARTESIAN_POINT('Ctrl Pts',(0.,-2.15109360305841,-7.70599703408915));
#45711=CARTESIAN_POINT('Ctrl Pts',(1.5,-2.15109360305841,-7.70599703408915));
#45712=CARTESIAN_POINT('Ctrl Pts',(0.,-2.01735309785409,-7.74208501985227));
#45713=CARTESIAN_POINT('Ctrl Pts',(1.5,-2.01735309785409,-7.74208501985227));
#45714=CARTESIAN_POINT('Ctrl Pts',(0.,-1.88300782832642,-7.77585207493021));
#45715=CARTESIAN_POINT('Ctrl Pts',(1.5,-1.88300782832642,-7.77585207493021));
#45716=CARTESIAN_POINT('Ctrl Pts',(0.,-1.74809806871328,-7.80728807684922));
#45717=CARTESIAN_POINT('Ctrl Pts',(1.5,-1.74809806871328,-7.80728807684922));
#45718=CARTESIAN_POINT('Ctrl Pts',(0.,-1.61266426241909,-7.83638360168719));
#45719=CARTESIAN_POINT('Ctrl Pts',(1.5,-1.61266426241909,-7.83638360168719));
#45720=CARTESIAN_POINT('Ctrl Pts',(0.,-1.47674700988627,-7.86312992690011));
#45721=CARTESIAN_POINT('Ctrl Pts',(1.5,-1.47674700988627,-7.86312992690011));
#45722=CARTESIAN_POINT('Ctrl Pts',(0.,-1.34038705647653,-7.88751903419248));
#45723=CARTESIAN_POINT('Ctrl Pts',(1.5,-1.34038705647653,-7.88751903419248));
#45724=CARTESIAN_POINT('Ctrl Pts',(0.,-1.20362528036119,-7.90954361243176));
#45725=CARTESIAN_POINT('Ctrl Pts',(1.5,-1.20362528036119,-7.90954361243176));
#45726=CARTESIAN_POINT('Ctrl Pts',(0.,-1.06650268017935,-7.92919705932551));
#45727=CARTESIAN_POINT('Ctrl Pts',(1.5,-1.06650268017935,-7.92919705932551));
#45728=CARTESIAN_POINT('Ctrl Pts',(0.,-0.929060362703573,-7.94647348314288));
#45729=CARTESIAN_POINT('Ctrl Pts',(1.5,-0.929060362703573,-7.94647348314288));
#45730=CARTESIAN_POINT('Ctrl Pts',(0.,-0.791339530512307,-7.96136770448042));
#45731=CARTESIAN_POINT('Ctrl Pts',(1.5,-0.791339530512307,-7.96136770448042));
#45732=CARTESIAN_POINT('Ctrl Pts',(0.,-0.653381469668319,-7.97387525807254));
#45733=CARTESIAN_POINT('Ctrl Pts',(1.5,-0.653381469668319,-7.97387525807254));
#45734=CARTESIAN_POINT('Ctrl Pts',(0.,-0.515227537402346,-7.98399239464636));
#45735=CARTESIAN_POINT('Ctrl Pts',(1.5,-0.515227537402346,-7.98399239464636));
#45736=CARTESIAN_POINT('Ctrl Pts',(0.,-0.376919149672593,-7.99171608152895));
#45737=CARTESIAN_POINT('Ctrl Pts',(1.5,-0.376919149672593,-7.99171608152895));
#45738=CARTESIAN_POINT('Ctrl Pts',(0.,-0.238497768727867,-7.99704400329913));
#45739=CARTESIAN_POINT('Ctrl Pts',(1.5,-0.238497768727867,-7.99704400329913));
#45740=CARTESIAN_POINT('Ctrl Pts',(0.,-0.100004890673634,-7.99997456248423));
#45741=CARTESIAN_POINT('Ctrl Pts',(1.5,-0.100004890673634,-7.99997456248423));
#45742=CARTESIAN_POINT('Ctrl Pts',(0.,0.0385179669597413,-8.00050688030175));
#45743=CARTESIAN_POINT('Ctrl Pts',(1.5,0.0385179669597413,-8.00050688030175));
#45744=CARTESIAN_POINT('Ctrl Pts',(0.,0.177029277647508,-7.99864079744583));
#45745=CARTESIAN_POINT('Ctrl Pts',(1.5,0.177029277647508,-7.99864079744583));
#45746=CARTESIAN_POINT('Ctrl Pts',(0.,0.31548751831724,-7.99437687360868));
#45747=CARTESIAN_POINT('Ctrl Pts',(1.5,0.31548751831724,-7.99437687360868));
#45748=CARTESIAN_POINT('Ctrl Pts',(0.,0.453851181795815,-7.98771638704679));
#45749=CARTESIAN_POINT('Ctrl Pts',(1.5,0.453851181795815,-7.98771638704679));
#45750=CARTESIAN_POINT('Ctrl Pts',(0.,0.59207878925734,-7.97866133419203));
#45751=CARTESIAN_POINT('Ctrl Pts',(1.5,0.59207878925734,-7.97866133419203));
#45752=CARTESIAN_POINT('Ctrl Pts',(0.,0.730128902672901,-7.9672144293078));
#45753=CARTESIAN_POINT('Ctrl Pts',(1.5,0.730128902672901,-7.9672144293078));
#45754=CARTESIAN_POINT('Ctrl Pts',(0.,0.867960137262859,-7.95337910418991));
#45755=CARTESIAN_POINT('Ctrl Pts',(1.5,0.867960137262859,-7.95337910418991));
#45756=CARTESIAN_POINT('Ctrl Pts',(0.,1.00553117385478,-7.9371595066318));
#45757=CARTESIAN_POINT('Ctrl Pts',(1.5,1.00553117385478,-7.9371595066318));
#45758=CARTESIAN_POINT('Ctrl Pts',(0.,1.14280077124549,-7.91856049893449));
#45759=CARTESIAN_POINT('Ctrl Pts',(1.5,1.14280077124549,-7.91856049893449));
#45760=CARTESIAN_POINT('Ctrl Pts',(0.,1.27972777856801,-7.89758765646115));
#45761=CARTESIAN_POINT('Ctrl Pts',(1.5,1.27972777856801,-7.89758765646115));
#45762=CARTESIAN_POINT('Ctrl Pts',(0.,1.41627114766405,-7.87424726623619));
#45763=CARTESIAN_POINT('Ctrl Pts',(1.5,1.41627114766405,-7.87424726623619));
#45764=CARTESIAN_POINT('Ctrl Pts',(0.,1.55238994546304,-7.8485463255889));
#45765=CARTESIAN_POINT('Ctrl Pts',(1.5,1.55238994546304,-7.8485463255889));
#45766=CARTESIAN_POINT('Ctrl Pts',(0.,1.68804336616293,-7.8204925395136));
#45767=CARTESIAN_POINT('Ctrl Pts',(1.5,1.68804336616293,-7.8204925395136));
#45768=CARTESIAN_POINT('Ctrl Pts',(0.,1.823190743419,-7.79009431807374));
#45769=CARTESIAN_POINT('Ctrl Pts',(1.5,1.823190743419,-7.79009431807374));
#45770=CARTESIAN_POINT('Ctrl Pts',(0.,1.95779156254127,-7.7573607738503));
#45771=CARTESIAN_POINT('Ctrl Pts',(1.5,1.95779156254127,-7.7573607738503));
#45772=CARTESIAN_POINT('Ctrl Pts',(0.,2.09180547270151,-7.72230171943405));
#45773=CARTESIAN_POINT('Ctrl Pts',(1.5,2.09180547270151,-7.72230171943405));
#45774=CARTESIAN_POINT('Ctrl Pts',(0.,2.22519229915041,-7.68492766496142));
#45775=CARTESIAN_POINT('Ctrl Pts',(1.5,2.22519229915041,-7.68492766496142));
#45776=CARTESIAN_POINT('Ctrl Pts',(0.,2.35791205512021,-7.6452498145298));
#45777=CARTESIAN_POINT('Ctrl Pts',(1.5,2.35791205512021,-7.6452498145298));
#45778=CARTESIAN_POINT('Ctrl Pts',(0.,2.48992495373911,-7.60328006265592));
#45779=CARTESIAN_POINT('Ctrl Pts',(1.5,2.48992495373911,-7.60328006265592));
#45780=CARTESIAN_POINT('Ctrl Pts',(0.,2.62119141995809,-7.55903099077771));
#45781=CARTESIAN_POINT('Ctrl Pts',(1.5,2.62119141995809,-7.55903099077771));
#45782=CARTESIAN_POINT('Ctrl Pts',(0.,2.75167210249111,-7.51251586379867));
#45783=CARTESIAN_POINT('Ctrl Pts',(1.5,2.75167210249111,-7.51251586379867));
#45784=CARTESIAN_POINT('Ctrl Pts',(0.,2.88132788576913,-7.4637486266753));
#45785=CARTESIAN_POINT('Ctrl Pts',(1.5,2.88132788576913,-7.4637486266753));
#45786=CARTESIAN_POINT('Ctrl Pts',(0.,3.01011990149821,-7.41274389958788));
#45787=CARTESIAN_POINT('Ctrl Pts',(1.5,3.01011990149821,-7.41274389958788));
#45788=CARTESIAN_POINT('Ctrl Pts',(0.,3.13800954023306,-7.35951697315347));
#45789=CARTESIAN_POINT('Ctrl Pts',(1.5,3.13800954023306,-7.35951697315347));
#45790=CARTESIAN_POINT('Ctrl Pts',(0.,3.26495846296673,-7.30408380368086));
#45791=CARTESIAN_POINT('Ctrl Pts',(1.5,3.26495846296673,-7.30408380368086));
#45792=CARTESIAN_POINT('Ctrl Pts',(0.,3.3909286127372,-7.24646100846717));
#45793=CARTESIAN_POINT('Ctrl Pts',(1.5,3.3909286127372,-7.24646100846717));
#45794=CARTESIAN_POINT('Ctrl Pts',(0.,3.51588222625169,-7.18666586113568));
#45795=CARTESIAN_POINT('Ctrl Pts',(1.5,3.51588222625169,-7.18666586113568));
#45796=CARTESIAN_POINT('Ctrl Pts',(0.,3.63978184496066,-7.12471628635636));
#45797=CARTESIAN_POINT('Ctrl Pts',(1.5,3.63978184496066,-7.12471628635636));
#45798=CARTESIAN_POINT('Ctrl Pts',(0.,3.76259032615096,-7.06063085460692));
#45799=CARTESIAN_POINT('Ctrl Pts',(1.5,3.76259032615096,-7.06063085460692));
#45800=CARTESIAN_POINT('Ctrl Pts',(0.,3.88427085405865,-6.99442877697438));
#45801=CARTESIAN_POINT('Ctrl Pts',(1.5,3.88427085405865,-6.99442877697438));
#45802=CARTESIAN_POINT('Ctrl Pts',(0.,4.00478695100224,-6.92612989999653));
#45803=CARTESIAN_POINT('Ctrl Pts',(1.5,4.00478695100224,-6.92612989999653));
#45804=CARTESIAN_POINT('Ctrl Pts',(0.,4.12410248853711,-6.85575470054316));
#45805=CARTESIAN_POINT('Ctrl Pts',(1.5,4.12410248853711,-6.85575470054316));
#45806=CARTESIAN_POINT('Ctrl Pts',(0.,4.24218169808549,-6.78332427836585));
#45807=CARTESIAN_POINT('Ctrl Pts',(1.5,4.24218169808549,-6.78332427836585));
#45808=CARTESIAN_POINT('Ctrl Pts',(0.,4.35898918158893,-6.70886034868655));
#45809=CARTESIAN_POINT('Ctrl Pts',(1.5,4.35898918158893,-6.70886034868655));
#45810=CARTESIAN_POINT('Ctrl Pts',(0.,4.47448992218382,-6.6323852348247));
#45811=CARTESIAN_POINT('Ctrl Pts',(1.5,4.47448992218382,-6.6323852348247));
#45812=CARTESIAN_POINT('Ctrl Pts',(0.,4.58864929490088,-6.55392186086227));
#45813=CARTESIAN_POINT('Ctrl Pts',(1.5,4.58864929490088,-6.55392186086227));
#45814=CARTESIAN_POINT('Ctrl Pts',(0.,4.70143307738904,-6.47349374434655));
#45815=CARTESIAN_POINT('Ctrl Pts',(1.5,4.70143307738904,-6.47349374434655));
#45816=CARTESIAN_POINT('Ctrl Pts',(0.,4.8128074597363,-6.39112499081239));
#45817=CARTESIAN_POINT('Ctrl Pts',(1.5,4.8128074597363,-6.39112499081239));
#45818=CARTESIAN_POINT('Ctrl Pts',(0.,4.92273905431645,-6.3068402883412));
#45819=CARTESIAN_POINT('Ctrl Pts',(1.5,4.92273905431645,-6.3068402883412));
#45820=CARTESIAN_POINT('Ctrl Pts',(0.,5.03119490566203,-6.22066490215631));
#45821=CARTESIAN_POINT('Ctrl Pts',(1.5,5.03119490566203,-6.22066490215631));
#45822=CARTESIAN_POINT('Ctrl Pts',(0.,5.13814250036441,-6.13262466925436));
#45823=CARTESIAN_POINT('Ctrl Pts',(1.5,5.13814250036441,-6.13262466925436));
#45824=CARTESIAN_POINT('Ctrl Pts',(0.,5.24354977700144,-6.04274599307227));
#45825=CARTESIAN_POINT('Ctrl Pts',(1.5,5.24354977700144,-6.04274599307227));
#45826=CARTESIAN_POINT('Ctrl Pts',(0.,5.34738513573851,-5.95105583052982));
#45827=CARTESIAN_POINT('Ctrl Pts',(1.5,5.34738513573851,-5.95105583052982));
#45828=CARTESIAN_POINT('Ctrl Pts',(0.,5.44961744795835,-5.85758167910657));
#45829=CARTESIAN_POINT('Ctrl Pts',(1.5,5.44961744795835,-5.85758167910657));
#45830=CARTESIAN_POINT('Ctrl Pts',(0.,5.55021606592032,-5.76235156395272));
#45831=CARTESIAN_POINT('Ctrl Pts',(1.5,5.55021606592032,-5.76235156395272));
#45832=CARTESIAN_POINT('Ctrl Pts',(0.,5.6491508324498,-5.66539402503311));
#45833=CARTESIAN_POINT('Ctrl Pts',(1.5,5.6491508324498,-5.66539402503311));
#45834=CARTESIAN_POINT('Ctrl Pts',(0.,5.74639209065813,-5.56673810430373));
#45835=CARTESIAN_POINT('Ctrl Pts',(1.5,5.74639209065813,-5.56673810430373));
#45836=CARTESIAN_POINT('Ctrl Pts',(0.,5.84191069171249,-5.46641334741991));
#45837=CARTESIAN_POINT('Ctrl Pts',(1.5,5.84191069171249,-5.46641334741991));
#45838=CARTESIAN_POINT('Ctrl Pts',(0.,5.93567800263758,-5.3644498054763));
#45839=CARTESIAN_POINT('Ctrl Pts',(1.5,5.93567800263758,-5.3644498054763));
#45840=CARTESIAN_POINT('Ctrl Pts',(0.,6.02766591414951,-5.26087803677827));
#45841=CARTESIAN_POINT('Ctrl Pts',(1.5,6.02766591414951,-5.26087803677827));
#45842=CARTESIAN_POINT('Ctrl Pts',(0.,6.11784684852245,-5.15572910864454));
#45843=CARTESIAN_POINT('Ctrl Pts',(1.5,6.11784684852245,-5.15572910864454));
#45844=CARTESIAN_POINT('Ctrl Pts',(0.,6.20619376748852,-5.04903459924103));
#45845=CARTESIAN_POINT('Ctrl Pts',(1.5,6.20619376748852,-5.04903459924103));
#45846=CARTESIAN_POINT('Ctrl Pts',(0.,6.29268018169352,-4.94082656273383));
#45847=CARTESIAN_POINT('Ctrl Pts',(1.5,6.29268018169352,-4.94082656273383));
#45848=CARTESIAN_POINT('Ctrl Pts',(0.,6.37728016018695,-4.83113749447141));
#45849=CARTESIAN_POINT('Ctrl Pts',(1.5,6.37728016018695,-4.83113749447141));
#45850=CARTESIAN_POINT('Ctrl Pts',(0.,6.45996833994694,-4.72000029619493));
#45851=CARTESIAN_POINT('Ctrl Pts',(1.5,6.45996833994694,-4.72000029619493));
#45852=CARTESIAN_POINT('Ctrl Pts',(0.,6.54071993544062,-4.60744824127475));
#45853=CARTESIAN_POINT('Ctrl Pts',(1.5,6.54071993544062,-4.60744824127475));
#45854=CARTESIAN_POINT('Ctrl Pts',(0.,6.61951074822048,-4.49351493997171));
#45855=CARTESIAN_POINT('Ctrl Pts',(1.5,6.61951074822048,-4.49351493997171));
#45856=CARTESIAN_POINT('Ctrl Pts',(0.,6.69631716969172,-4.37823438722894));
#45857=CARTESIAN_POINT('Ctrl Pts',(1.5,6.69631716969172,-4.37823438722894));
#45858=CARTESIAN_POINT('Ctrl Pts',(0.,6.77111618391648,-4.26164101048826));
#45859=CARTESIAN_POINT('Ctrl Pts',(1.5,6.77111618391648,-4.26164101048826));
#45860=CARTESIAN_POINT('Ctrl Pts',(0.,6.84388537045513,-4.14376971753304));
#45861=CARTESIAN_POINT('Ctrl Pts',(1.5,6.84388537045513,-4.14376971753304));
#45862=CARTESIAN_POINT('Ctrl Pts',(0.,6.91460290724495,-4.02465594435878));
#45863=CARTESIAN_POINT('Ctrl Pts',(1.5,6.91460290724495,-4.02465594435878));
#45864=CARTESIAN_POINT('Ctrl Pts',(0.,6.98324757351635,-3.90433570307326));
#45865=CARTESIAN_POINT('Ctrl Pts',(1.5,6.98324757351635,-3.90433570307326));
#45866=CARTESIAN_POINT('Ctrl Pts',(0.,7.04979876513603,-3.78284543574385));
#45867=CARTESIAN_POINT('Ctrl Pts',(1.5,7.04979876513603,-3.78284543574385));
#45868=CARTESIAN_POINT('Ctrl Pts',(0.,7.11423650998851,-3.66022186827001));
#45869=CARTESIAN_POINT('Ctrl Pts',(1.5,7.11423650998851,-3.66022186827001));
#45870=CARTESIAN_POINT('Ctrl Pts',(0.,7.17654148339738,-3.53650186427521));
#45871=CARTESIAN_POINT('Ctrl Pts',(1.5,7.17654148339738,-3.53650186427521));
#45872=CARTESIAN_POINT('Ctrl Pts',(0.,7.23669502358634,-3.41172227901257));
#45873=CARTESIAN_POINT('Ctrl Pts',(1.5,7.23669502358634,-3.41172227901257));
#45874=CARTESIAN_POINT('Ctrl Pts',(0.,7.29467914718136,-3.28591981327804));
#45875=CARTESIAN_POINT('Ctrl Pts',(1.5,7.29467914718136,-3.28591981327804));
#45876=CARTESIAN_POINT('Ctrl Pts',(0.,7.350476532226,-3.15913131592765));
#45877=CARTESIAN_POINT('Ctrl Pts',(1.5,7.350476532226,-3.15913131592765));
#45878=CARTESIAN_POINT('Ctrl Pts',(0.,7.40407050123789,-3.03139408640772));
#45879=CARTESIAN_POINT('Ctrl Pts',(1.5,7.40407050123789,-3.03139408640772));
#45880=CARTESIAN_POINT('Ctrl Pts',(0.,7.45544500430585,-2.90274617730943));
#45881=CARTESIAN_POINT('Ctrl Pts',(1.5,7.45544500430585,-2.90274617730943));
#45882=CARTESIAN_POINT('Ctrl Pts',(0.,7.5045846022269,-2.7732266969588));
#45883=CARTESIAN_POINT('Ctrl Pts',(1.5,7.5045846022269,-2.7732266969588));
#45884=CARTESIAN_POINT('Ctrl Pts',(0.,7.55147444968283,-2.64287611205352));
#45885=CARTESIAN_POINT('Ctrl Pts',(1.5,7.55147444968283,-2.64287611205352));
#45886=CARTESIAN_POINT('Ctrl Pts',(0.,7.5961003500545,-2.51173550715636));
#45887=CARTESIAN_POINT('Ctrl Pts',(1.5,7.5961003500545,-2.51173550715636));
#45888=CARTESIAN_POINT('Ctrl Pts',(0.,7.638448810277,-2.37984584421852));
#45889=CARTESIAN_POINT('Ctrl Pts',(1.5,7.638448810277,-2.37984584421852));
#45890=CARTESIAN_POINT('Ctrl Pts',(0.,7.67850709573841,-2.24724722210384));
#45891=CARTESIAN_POINT('Ctrl Pts',(1.5,7.67850709573841,-2.24724722210384));
#45892=CARTESIAN_POINT('Ctrl Pts',(0.,7.71626328522396,-2.11397813608674));
#45893=CARTESIAN_POINT('Ctrl Pts',(1.5,7.71626328522396,-2.11397813608674));
#45894=CARTESIAN_POINT('Ctrl Pts',(0.,7.75170632590802,-1.98007473729369));
#45895=CARTESIAN_POINT('Ctrl Pts',(1.5,7.75170632590802,-1.98007473729369));
#45896=CARTESIAN_POINT('Ctrl Pts',(0.,7.78482591855345,-1.84557250184578));
#45897=CARTESIAN_POINT('Ctrl Pts',(1.5,7.78482591855345,-1.84557250184578));
#45898=CARTESIAN_POINT('Ctrl Pts',(0.,7.81561240275672,-1.71050789997943));
#45899=CARTESIAN_POINT('Ctrl Pts',(1.5,7.81561240275672,-1.71050789997943));
#45900=CARTESIAN_POINT('Ctrl Pts',(0.,7.84405664223427,-1.57492006520963));
#45901=CARTESIAN_POINT('Ctrl Pts',(1.5,7.84405664223427,-1.57492006520963));
#45902=CARTESIAN_POINT('Ctrl Pts',(0.,7.87014991014611,-1.43885246359668));
#45903=CARTESIAN_POINT('Ctrl Pts',(1.5,7.87014991014611,-1.43885246359668));
#45904=CARTESIAN_POINT('Ctrl Pts',(0.,7.89388377445188,-1.30235456318281));
#45905=CARTESIAN_POINT('Ctrl Pts',(1.5,7.89388377445188,-1.30235456318281));
#45906=CARTESIAN_POINT('Ctrl Pts',(0.,7.91525036159865,-1.16547817540872));
#45907=CARTESIAN_POINT('Ctrl Pts',(1.5,7.91525036159865,-1.16547817540872));
#45908=CARTESIAN_POINT('Ctrl Pts',(0.,7.93424262024687,-1.0282737966247));
#45909=CARTESIAN_POINT('Ctrl Pts',(1.5,7.93424262024687,-1.0282737966247));
#45910=CARTESIAN_POINT('Ctrl Pts',(0.,7.95085458504517,-0.890786949553448));
#45911=CARTESIAN_POINT('Ctrl Pts',(1.5,7.95085458504517,-0.890786949553448));
#45912=CARTESIAN_POINT('Ctrl Pts',(0.,7.96508164046348,-0.753054524569566));
#45913=CARTESIAN_POINT('Ctrl Pts',(1.5,7.96508164046348,-0.753054524569566));
#45914=CARTESIAN_POINT('Ctrl Pts',(0.,7.97692078469519,-0.615101120652533));
#45915=CARTESIAN_POINT('Ctrl Pts',(1.5,7.97692078469519,-0.615101120652533));
#45916=CARTESIAN_POINT('Ctrl Pts',(0.,7.98637028879241,-0.476941502740932));
#45917=CARTESIAN_POINT('Ctrl Pts',(1.5,7.98637028879241,-0.476941502740932));
#45918=CARTESIAN_POINT('Ctrl Pts',(0.,7.99201754245236,-0.366254747519825));
#45919=CARTESIAN_POINT('Ctrl Pts',(1.5,7.99201754245236,-0.366254747519825));
#45920=CARTESIAN_POINT('Ctrl Pts',(0.,7.99517719352919,-0.283151319739979));
#45921=CARTESIAN_POINT('Ctrl Pts',(1.5,7.99517719352919,-0.283151319739979));
#45922=CARTESIAN_POINT('Ctrl Pts',(0.,7.9968055050659,-0.227709763329173));
#45923=CARTESIAN_POINT('Ctrl Pts',(1.5,7.9968055050659,-0.227709763329173));
#45924=CARTESIAN_POINT('Ctrl Pts',(0.,7.99750013020562,-0.199979167317696));
#45925=CARTESIAN_POINT('Ctrl Pts',(1.5,7.99750013020562,-0.199979167317696));
#45926=CARTESIAN_POINT('',(0.15,7.99750013020562,0.199979167317619));
#45927=CARTESIAN_POINT('',(0.,7.99750013020562,0.199979167317699));
#45928=CARTESIAN_POINT('Ctrl Pts',(0.15,7.99749996249466,-0.19998586250798));
#45929=CARTESIAN_POINT('Ctrl Pts',(0.15,7.961995738416,-1.61732659559412));
#45930=CARTESIAN_POINT('Ctrl Pts',(0.15,7.12114441317228,-4.42734848781943));
#45931=CARTESIAN_POINT('Ctrl Pts',(0.15,3.90389095991274,-7.41867892302632));
#45932=CARTESIAN_POINT('Ctrl Pts',(0.15,-1.06985836751423,-8.53832254812639));
#45933=CARTESIAN_POINT('Ctrl Pts',(0.15,-6.34173425813201,-6.08127940476401));
#45934=CARTESIAN_POINT('Ctrl Pts',(0.15,-8.7127134194499,-0.24784357163776));
#45935=CARTESIAN_POINT('Ctrl Pts',(0.15,-6.73863305333642,5.52529506822021));
#45936=CARTESIAN_POINT('Ctrl Pts',(0.15,-3.09413630122569,7.64282159505089));
#45937=CARTESIAN_POINT('Ctrl Pts',(0.15,0.396398773959542,8.13986317370034));
#45938=CARTESIAN_POINT('Ctrl Pts',(0.15,3.56795524744049,7.62772577919895));
#45939=CARTESIAN_POINT('Ctrl Pts',(0.15,7.04944249732077,4.60837388453871));
#45940=CARTESIAN_POINT('Ctrl Pts',(0.15,7.96045345605701,1.67894428791899));
#45941=CARTESIAN_POINT('Ctrl Pts',(0.15,7.99750013020563,0.19997916731746));
#45942=CARTESIAN_POINT('Ctrl Pts',(0.15,7.99750013020563,0.19997916731746));
#45943=CARTESIAN_POINT('Ctrl Pts',(0.15,7.96045345605701,1.67894428791899));
#45944=CARTESIAN_POINT('Ctrl Pts',(0.15,7.04944249732077,4.60837388453871));
#45945=CARTESIAN_POINT('Ctrl Pts',(0.15,3.56795524744049,7.62772577919895));
#45946=CARTESIAN_POINT('Ctrl Pts',(0.15,0.396398773959542,8.13986317370034));
#45947=CARTESIAN_POINT('Ctrl Pts',(0.15,-3.09413630122569,7.64282159505089));
#45948=CARTESIAN_POINT('Ctrl Pts',(0.15,-6.73863305333642,5.52529506822021));
#45949=CARTESIAN_POINT('Ctrl Pts',(0.15,-8.7127134194499,-0.24784357163776));
#45950=CARTESIAN_POINT('Ctrl Pts',(0.15,-6.34173425813201,-6.08127940476401));
#45951=CARTESIAN_POINT('Ctrl Pts',(0.15,-1.06985836751423,-8.53832254812639));
#45952=CARTESIAN_POINT('Ctrl Pts',(0.15,3.90389095991274,-7.41867892302632));
#45953=CARTESIAN_POINT('Ctrl Pts',(0.15,7.12114441317228,-4.42734848781943));
#45954=CARTESIAN_POINT('Ctrl Pts',(0.15,7.961995738416,-1.61732659559412));
#45955=CARTESIAN_POINT('Ctrl Pts',(0.15,7.99749996249466,-0.19998586250798));
#45956=CARTESIAN_POINT('Ctrl Pts',(0.1,7.94751580920271,0.19872710746362));
#45957=CARTESIAN_POINT('Ctrl Pts',(0.0999999999999999,7.91068175784103,
1.66845202534325));
#45958=CARTESIAN_POINT('Ctrl Pts',(0.1,7.00539776889503,4.57959570636687));
#45959=CARTESIAN_POINT('Ctrl Pts',(0.1,3.54564541349769,7.58002805922958));
#45960=CARTESIAN_POINT('Ctrl Pts',(0.1,0.393922023965292,8.08901822676633));
#45961=CARTESIAN_POINT('Ctrl Pts',(0.1,-3.07480005979067,7.59502792370097));
#45962=CARTESIAN_POINT('Ctrl Pts',(0.1,-6.69651470180966,5.49077279428345));
#45963=CARTESIAN_POINT('Ctrl Pts',(0.1,-8.65825783268014,-0.246297266556145));
#45964=CARTESIAN_POINT('Ctrl Pts',(0.1,-6.30209920788036,-6.04327542832943));
#45965=CARTESIAN_POINT('Ctrl Pts',(0.1,-1.06317179958156,-8.48494793422131));
#45966=CARTESIAN_POINT('Ctrl Pts',(0.1,3.87948800454988,-7.37234199492993));
#45967=CARTESIAN_POINT('Ctrl Pts',(0.1,7.07664686572023,-4.39964468727081));
#45968=CARTESIAN_POINT('Ctrl Pts',(0.1,7.91220940446938,-1.60725513423082));
#45969=CARTESIAN_POINT('Ctrl Pts',(0.1,7.94751564253563,-0.198733760980932));
#45970=CARTESIAN_POINT('Ctrl Pts',(0.05,7.8975314881998,0.19747504760978));
#45971=CARTESIAN_POINT('Ctrl Pts',(0.0500000000000001,7.86096398282589,
1.6580628961152));
#45972=CARTESIAN_POINT('Ctrl Pts',(0.0499999999999999,6.96130852626912,
4.55073165493979));
#45973=CARTESIAN_POINT('Ctrl Pts',(0.0500000000000001,3.52336618735535,
7.53242134786548));
#45974=CARTESIAN_POINT('Ctrl Pts',(0.05,0.391442899960782,8.03808465462494));
#45975=CARTESIAN_POINT('Ctrl Pts',(0.05,-3.05545752250296,7.54731294656525));
#45976=CARTESIAN_POINT('Ctrl Pts',(0.05,-6.6544020560685,5.45621682823237));
#45977=CARTESIAN_POINT('Ctrl Pts',(0.05,-8.60380561359923,-0.244740933791259));
#45978=CARTESIAN_POINT('Ctrl Pts',(0.05,-6.26246183682716,-6.00526335382877));
#45979=CARTESIAN_POINT('Ctrl Pts',(0.05,-1.05648506055284,-8.43159806974257));
#45980=CARTESIAN_POINT('Ctrl Pts',(0.05,3.85509562628092,-7.32593505111813));
#45981=CARTESIAN_POINT('Ctrl Pts',(0.05,7.0321200317712,-4.37201968712336));
#45982=CARTESIAN_POINT('Ctrl Pts',(0.05,7.86249210118029,-1.59717501758574));
#45983=CARTESIAN_POINT('Ctrl Pts',(0.05,7.89753132257661,-0.197481659453884));
#45984=CARTESIAN_POINT('Ctrl Pts',(0.,7.84754716719688,0.19622298775594));
#45985=CARTESIAN_POINT('Ctrl Pts',(0.,7.81119228460991,1.64757063353946));
#45986=CARTESIAN_POINT('Ctrl Pts',(0.,6.91726379784338,4.52195347676795));
#45987=CARTESIAN_POINT('Ctrl Pts',(0.,3.50105635341255,7.48472362789611));
#45988=CARTESIAN_POINT('Ctrl Pts',(0.,0.388966149966533,7.98723970769094));
#45989=CARTESIAN_POINT('Ctrl Pts',(0.,-3.03612128106794,7.49951927521533));
#45990=CARTESIAN_POINT('Ctrl Pts',(0.,-6.61228370454174,5.42169455429562));
#45991=CARTESIAN_POINT('Ctrl Pts',(0.,-8.54935002682948,-0.243194628709643));
#45992=CARTESIAN_POINT('Ctrl Pts',(0.,-6.22282678657551,-5.96725937739419));
#45993=CARTESIAN_POINT('Ctrl Pts',(0.,-1.04979849262017,-8.37822345583749));
#45994=CARTESIAN_POINT('Ctrl Pts',(0.,3.83069267091806,-7.27959812302174));
#45995=CARTESIAN_POINT('Ctrl Pts',(0.,6.98762248431915,-4.34431588657474));
#45996=CARTESIAN_POINT('Ctrl Pts',(0.,7.81270576723367,-1.58710355622244));
#45997=CARTESIAN_POINT('Ctrl Pts',(0.,7.84754700261759,-0.196229557926836));
#45998=CARTESIAN_POINT('',(0.,7.84754700261759,0.196229557926824));
#45999=CARTESIAN_POINT('Ctrl Pts',(0.15,7.99750013020562,0.199979167317699));
#46000=CARTESIAN_POINT('Ctrl Pts',(0.1,7.94751580920271,0.198727107463857));
#46001=CARTESIAN_POINT('Ctrl Pts',(0.05,7.89753148819979,0.197475047610016));
#46002=CARTESIAN_POINT('Ctrl Pts',(0.,7.84754716719688,0.196222987756174));
#46003=CARTESIAN_POINT('Ctrl Pts',(0.,7.84754700261752,0.196229557926955));
#46004=CARTESIAN_POINT('Ctrl Pts',(0.,7.81119093568739,1.64757497093006));
#46005=CARTESIAN_POINT('Ctrl Pts',(0.,6.91726207951188,4.52195496702326));
#46006=CARTESIAN_POINT('Ctrl Pts',(0.,3.50105635341255,7.48472362789611));
#46007=CARTESIAN_POINT('Ctrl Pts',(0.,0.388966149966533,7.98723970769094));
#46008=CARTESIAN_POINT('Ctrl Pts',(0.,-3.03612128106794,7.49951927521533));
#46009=CARTESIAN_POINT('Ctrl Pts',(0.,-6.61228370454174,5.42169455429562));
#46010=CARTESIAN_POINT('Ctrl Pts',(0.,-8.54935002682948,-0.243194628709643));
#46011=CARTESIAN_POINT('Ctrl Pts',(0.,-6.22282678657551,-5.96725937739419));
#46012=CARTESIAN_POINT('Ctrl Pts',(0.,-1.04979849262017,-8.37822345583749));
#46013=CARTESIAN_POINT('Ctrl Pts',(0.,3.83069267091806,-7.27959812302174));
#46014=CARTESIAN_POINT('Ctrl Pts',(0.,6.98762248431915,-4.34431588657474));
#46015=CARTESIAN_POINT('Ctrl Pts',(0.,7.81270576723367,-1.58710355622244));
#46016=CARTESIAN_POINT('Ctrl Pts',(0.,7.84754700261759,-0.196229557926836));
#46017=CARTESIAN_POINT('Ctrl Pts',(1.5,7.04779698988764,-0.176231641202319));
#46018=CARTESIAN_POINT('Ctrl Pts',(1.5,7.04679841138751,-0.216096563028019));
#46019=CARTESIAN_POINT('Ctrl Pts',(1.5,7.02210915861748,-0.950460970728723));
#46020=CARTESIAN_POINT('Ctrl Pts',(1.5,6.73567311075118,-2.4431876756519));
#46021=CARTESIAN_POINT('Ctrl Pts',(1.5,6.00262529198976,-3.78210604931351));
#46022=CARTESIAN_POINT('Ctrl Pts',(1.5,5.26585512838814,-4.70378009980091));
#46023=CARTESIAN_POINT('Ctrl Pts',(1.5,4.81558620855694,-5.17668232873438));
#46024=CARTESIAN_POINT('Ctrl Pts',(1.50000000000001,4.30870466570876,-5.58661807788342));
#46025=CARTESIAN_POINT('Ctrl Pts',(1.5,3.97740575868414,-5.82285201212594));
#46026=CARTESIAN_POINT('Ctrl Pts',(1.5,3.11208933639409,-6.39613745229425));
#46027=CARTESIAN_POINT('Ctrl Pts',(1.5,1.33885201664721,-7.0889077154724));
#46028=CARTESIAN_POINT('Ctrl Pts',(1.5,-1.68411245569617,-7.09281159181233));
#46029=CARTESIAN_POINT('Ctrl Pts',(1.5,-4.62775288425511,-5.68940118968998));
#46030=CARTESIAN_POINT('Ctrl Pts',(1.5,-6.32134574348598,-3.41161455311364));
#46031=CARTESIAN_POINT('Ctrl Pts',(1.5,-7.16221072057386,-0.803465361099522));
#46032=CARTESIAN_POINT('Ctrl Pts',(1.5,-7.02869221054055,2.3863506274691));
#46033=CARTESIAN_POINT('Ctrl Pts',(1.5,-5.37642314477699,4.81506856485811));
#46034=CARTESIAN_POINT('Ctrl Pts',(1.5,-3.72631177636962,6.00861903758754));
#46035=CARTESIAN_POINT('Ctrl Pts',(1.5,-3.15225899889574,6.32066033764087));
#46036=CARTESIAN_POINT('Ctrl Pts',(1.5,-1.99143161293444,6.81376111970392));
#46037=CARTESIAN_POINT('Ctrl Pts',(1.5,0.487779908623596,7.37998777732575));
#46038=CARTESIAN_POINT('Ctrl Pts',(1.5,4.65659822313403,6.07462569563999));
#46039=CARTESIAN_POINT('Ctrl Pts',(1.5,6.69920345996918,2.86157096981349));
#46040=CARTESIAN_POINT('Ctrl Pts',(1.5,7.01651072249489,0.785791900119064));
#46041=CARTESIAN_POINT('Ctrl Pts',(1.5,7.04371625681567,0.339141322789337));
#46042=CARTESIAN_POINT('Ctrl Pts',(1.5,7.04779682531124,0.17623821136714));
#46043=CARTESIAN_POINT('Ctrl Pts',(1.45,6.99781266888479,-0.174979581345908));
#46044=CARTESIAN_POINT('Ctrl Pts',(1.45,6.99682147563086,-0.214557224352159));
#46045=CARTESIAN_POINT('Ctrl Pts',(1.45,6.97230420129675,-0.943733162635674));
#46046=CARTESIAN_POINT('Ctrl Pts',(1.45,6.68790467738006,-2.42585669145555));
#46047=CARTESIAN_POINT('Ctrl Pts',(1.45,5.96005079855331,-3.75528320175119));
#46048=CARTESIAN_POINT('Ctrl Pts',(1.45,5.22851006715451,-4.67042136148825));
#46049=CARTESIAN_POINT('Ctrl Pts',(1.45,4.78143238941665,-5.13996980373977));
#46050=CARTESIAN_POINT('Ctrl Pts',(1.45000000000001,4.27814675891659,-5.54699633461483));
#46051=CARTESIAN_POINT('Ctrl Pts',(1.45,3.94919749215172,-5.78155720403649));
#46052=CARTESIAN_POINT('Ctrl Pts',(1.45,3.09001661915318,-6.35076805597684));
#46053=CARTESIAN_POINT('Ctrl Pts',(1.45,1.32935731991496,-7.03863662198873));
#46054=CARTESIAN_POINT('Ctrl Pts',(1.45,-1.67216942797454,-7.04250475985423));
#46055=CARTESIAN_POINT('Ctrl Pts',(1.45,-4.59492940793848,-5.64905133658995));
#46056=CARTESIAN_POINT('Ctrl Pts',(1.45,-6.2765164025017,-3.387419573102));
#46057=CARTESIAN_POINT('Ctrl Pts',(1.45,-7.11141233623102,-0.797768988290111));
#46058=CARTESIAN_POINT('Ctrl Pts',(1.45,-6.97885055702535,2.36943805784273));
#46059=CARTESIAN_POINT('Ctrl Pts',(1.45,-5.33827403269554,4.7808924535148));
#46060=CARTESIAN_POINT('Ctrl Pts',(1.45,-3.69989160340351,5.96601615936688));
#46061=CARTESIAN_POINT('Ctrl Pts',(1.45,-3.12990393400893,6.27581629241273));
#46062=CARTESIAN_POINT('Ctrl Pts',(1.45,-1.97730629927358,6.76546702941564));
#46063=CARTESIAN_POINT('Ctrl Pts',(1.45,0.484310761962725,7.32762492052164));
#46064=CARTESIAN_POINT('Ctrl Pts',(1.45,4.62359284627412,6.03155923010541));
#46065=CARTESIAN_POINT('Ctrl Pts',(1.45,6.65165743453235,2.84126958716708));
#46066=CARTESIAN_POINT('Ctrl Pts',(1.45,6.96676461290019,0.780220626486363));
#46067=CARTESIAN_POINT('Ctrl Pts',(1.45,6.99374990469182,0.336735818412981));
#46068=CARTESIAN_POINT('Ctrl Pts',(1.45,6.99781250430828,0.174986151515265));
#46069=CARTESIAN_POINT('Ctrl Pts',(1.4,6.94782834788194,-0.173727521489497));
#46070=CARTESIAN_POINT('Ctrl Pts',(1.4,6.94682238413562,-0.213879722134646));
#46071=CARTESIAN_POINT('Ctrl Pts',(1.4,6.92253452269999,-0.935880701452195));
#46072=CARTESIAN_POINT('Ctrl Pts',(1.4,6.64011424361582,-2.40913955069607));
#46073=CARTESIAN_POINT('Ctrl Pts',(1.4,5.91748619336573,-3.7283597794975));
#46074=CARTESIAN_POINT('Ctrl Pts',(1.4,5.19116104062186,-4.63701500758754));
#46075=CARTESIAN_POINT('Ctrl Pts',(1.4,4.74728136227759,-5.10321492888003));
#46076=CARTESIAN_POINT('Ctrl Pts',(1.4,4.24758832208607,-5.50734849491544));
#46077=CARTESIAN_POINT('Ctrl Pts',(1.4,3.92098870849758,-5.74022965314134));
#46078=CARTESIAN_POINT('Ctrl Pts',(1.4,3.06794764178653,-6.30539534847945));
#46079=CARTESIAN_POINT('Ctrl Pts',(1.4,1.31986057164665,-6.98834485012048));
#46080=CARTESIAN_POINT('Ctrl Pts',(1.4,-1.66022325421088,-6.99220276121136));
#46081=CARTESIAN_POINT('Ctrl Pts',(1.4,-4.56211352938548,-5.60870006630621));
#46082=CARTESIAN_POINT('Ctrl Pts',(1.4,-6.23167836095184,-3.36322153640607));
#46083=CARTESIAN_POINT('Ctrl Pts',(1.4,-7.06062164022606,-0.792066687527311));
#46084=CARTESIAN_POINT('Ctrl Pts',(1.4,-6.92898721977216,2.35248988333773));
#46085=CARTESIAN_POINT('Ctrl Pts',(1.4,-5.30018025186195,4.74679632662372));
#46086=CARTESIAN_POINT('Ctrl Pts',(1.4,-3.67344868840864,5.9233788475635));
#46087=CARTESIAN_POINT('Ctrl Pts',(1.4,-3.10754468665178,6.2310221356181));
#46088=CARTESIAN_POINT('Ctrl Pts',(1.4,-1.96318596506224,6.71708128064611));
#46089=CARTESIAN_POINT('Ctrl Pts',(1.4,0.480870252832169,7.27533268572036));
#46090=CARTESIAN_POINT('Ctrl Pts',(1.4,4.59052892370703,5.98843660249075));
#46091=CARTESIAN_POINT('Ctrl Pts',(1.4,6.60421294758832,2.82099443701422));
#46092=CARTESIAN_POINT('Ctrl Pts',(1.4,6.9169695694088,0.774639474633935));
#46093=CARTESIAN_POINT('Ctrl Pts',(1.4,6.94381611987581,0.334338463253306));
#46094=CARTESIAN_POINT('Ctrl Pts',(1.4,6.94782818330531,0.17373409166339));
#46095=CARTESIAN_POINT('Ctrl Pts',(1.35,6.89784402687909,-0.172475461633086));
#46096=CARTESIAN_POINT('Ctrl Pts',(1.35,6.89684544837896,-0.212340383458786));
#46097=CARTESIAN_POINT('Ctrl Pts',(1.35,6.87272956537927,-0.929152893359146));
#46098=CARTESIAN_POINT('Ctrl Pts',(1.35,6.5923458102447,-2.39180856649973));
#46099=CARTESIAN_POINT('Ctrl Pts',(1.35,5.87491169992928,-3.70153693193518));
#46100=CARTESIAN_POINT('Ctrl Pts',(1.35,5.15381597938823,-4.60365626927488));
#46101=CARTESIAN_POINT('Ctrl Pts',(1.35,4.7131275431373,-5.06650240388542));
#46102=CARTESIAN_POINT('Ctrl Pts',(1.35,4.2170304152939,-5.46772675164685));
#46103=CARTESIAN_POINT('Ctrl Pts',(1.35,3.89278044196515,-5.69893484505189));
#46104=CARTESIAN_POINT('Ctrl Pts',(1.35,3.04587492454562,-6.26002595216204));
#46105=CARTESIAN_POINT('Ctrl Pts',(1.35,1.3103658749144,-6.93807375663681));
#46106=CARTESIAN_POINT('Ctrl Pts',(1.35,-1.64828022648925,-6.94189592925327));
#46107=CARTESIAN_POINT('Ctrl Pts',(1.35,-4.52929005306886,-5.56835021320618));
#46108=CARTESIAN_POINT('Ctrl Pts',(1.35,-6.18684901996756,-3.33902655639443));
#46109=CARTESIAN_POINT('Ctrl Pts',(1.35,-7.00982325588322,-0.7863703147179));
#46110=CARTESIAN_POINT('Ctrl Pts',(1.35,-6.87914556625695,2.33557731371137));
#46111=CARTESIAN_POINT('Ctrl Pts',(1.35,-5.2620311397805,4.71262021528042));
#46112=CARTESIAN_POINT('Ctrl Pts',(1.35,-3.64702851544254,5.88077596934284));
#46113=CARTESIAN_POINT('Ctrl Pts',(1.35,-3.08518962176498,6.18617809038997));
#46114=CARTESIAN_POINT('Ctrl Pts',(1.35,-1.94906065140137,6.66878719035783));
#46115=CARTESIAN_POINT('Ctrl Pts',(1.35,0.477401106171298,7.22296982891625));
#46116=CARTESIAN_POINT('Ctrl Pts',(1.35,4.55752354684712,5.94537013695617));
#46117=CARTESIAN_POINT('Ctrl Pts',(1.35,6.5566669221515,2.80069305436781));
#46118=CARTESIAN_POINT('Ctrl Pts',(1.35,6.86722345981409,0.769068201001234));
#46119=CARTESIAN_POINT('Ctrl Pts',(1.35,6.89384976775196,0.33193295887695));
#46120=CARTESIAN_POINT('Ctrl Pts',(1.35,6.89784386230235,0.172482031811515));
#46121=CARTESIAN_POINT('',(1.35,6.89784386230235,0.172482031811515));
#46122=CARTESIAN_POINT('',(1.5,7.0477969074555,0.176234926281131));
#46123=CARTESIAN_POINT('Ctrl Pts',(1.35,6.89784386230235,0.172482031811515));
#46124=CARTESIAN_POINT('Ctrl Pts',(1.4,6.94782818330531,0.17373409166339));
#46125=CARTESIAN_POINT('Ctrl Pts',(1.45,6.99781250430828,0.174986151515265));
#46126=CARTESIAN_POINT('Ctrl Pts',(1.5,7.04779682531124,0.17623821136714));
#46127=CARTESIAN_POINT('Ctrl Pts',(1.5,7.04779682531124,0.17623821136714));
#46128=CARTESIAN_POINT('Ctrl Pts',(1.5,7.04371625681567,0.339141322789337));
#46129=CARTESIAN_POINT('Ctrl Pts',(1.5,7.01651072249489,0.785791900119064));
#46130=CARTESIAN_POINT('Ctrl Pts',(1.5,6.69920345996918,2.86157096981349));
#46131=CARTESIAN_POINT('Ctrl Pts',(1.5,4.65659822313403,6.07462569563999));
#46132=CARTESIAN_POINT('Ctrl Pts',(1.5,0.487779908623596,7.37998777732575));
#46133=CARTESIAN_POINT('Ctrl Pts',(1.5,-1.99143161293444,6.81376111970392));
#46134=CARTESIAN_POINT('Ctrl Pts',(1.5,-3.15225899889574,6.32066033764087));
#46135=CARTESIAN_POINT('Ctrl Pts',(1.5,-3.72631177636962,6.00861903758754));
#46136=CARTESIAN_POINT('Ctrl Pts',(1.5,-5.37642314477699,4.81506856485811));
#46137=CARTESIAN_POINT('Ctrl Pts',(1.5,-7.02869221054055,2.3863506274691));
#46138=CARTESIAN_POINT('Ctrl Pts',(1.5,-7.16221072057386,-0.803465361099522));
#46139=CARTESIAN_POINT('Ctrl Pts',(1.5,-6.32134574348598,-3.41161455311364));
#46140=CARTESIAN_POINT('Ctrl Pts',(1.5,-4.62775288425511,-5.68940118968998));
#46141=CARTESIAN_POINT('Ctrl Pts',(1.5,-1.68411245569617,-7.09281159181233));
#46142=CARTESIAN_POINT('Ctrl Pts',(1.5,1.33885201664721,-7.0889077154724));
#46143=CARTESIAN_POINT('Ctrl Pts',(1.5,3.11208933639409,-6.39613745229425));
#46144=CARTESIAN_POINT('Ctrl Pts',(1.5,3.97740575868414,-5.82285201212594));
#46145=CARTESIAN_POINT('Ctrl Pts',(1.50000000000001,4.30870466570876,-5.58661807788342));
#46146=CARTESIAN_POINT('Ctrl Pts',(1.5,4.81558620855694,-5.17668232873438));
#46147=CARTESIAN_POINT('Ctrl Pts',(1.5,5.26585512838814,-4.70378009980091));
#46148=CARTESIAN_POINT('Ctrl Pts',(1.5,6.00262529198976,-3.78210604931351));
#46149=CARTESIAN_POINT('Ctrl Pts',(1.5,6.73567311075118,-2.4431876756519));
#46150=CARTESIAN_POINT('Ctrl Pts',(1.5,7.02210915861748,-0.950460970728723));
#46151=CARTESIAN_POINT('Ctrl Pts',(1.5,7.04679841138751,-0.216096563028019));
#46152=CARTESIAN_POINT('Ctrl Pts',(1.5,7.04779698988764,-0.176231641202319));
#46153=CARTESIAN_POINT('Ctrl Pts',(1.35,6.89784386229926,-0.172482031811152));
#46154=CARTESIAN_POINT('Ctrl Pts',(1.35,6.89684530116423,-0.212344759189508));
#46155=CARTESIAN_POINT('Ctrl Pts',(1.35,6.87272914904771,-0.929155065202924));
#46156=CARTESIAN_POINT('Ctrl Pts',(1.35,6.5923458102447,-2.39180856649973));
#46157=CARTESIAN_POINT('Ctrl Pts',(1.35,5.87491169992928,-3.70153693193518));
#46158=CARTESIAN_POINT('Ctrl Pts',(1.35,5.15381597938823,-4.60365626927488));
#46159=CARTESIAN_POINT('Ctrl Pts',(1.35,4.7131275431373,-5.06650240388542));
#46160=CARTESIAN_POINT('Ctrl Pts',(1.35,4.2170304152939,-5.46772675164685));
#46161=CARTESIAN_POINT('Ctrl Pts',(1.35,3.89278044196515,-5.69893484505189));
#46162=CARTESIAN_POINT('Ctrl Pts',(1.35,3.04587492454562,-6.26002595216204));
#46163=CARTESIAN_POINT('Ctrl Pts',(1.35,1.3103658749144,-6.93807375663681));
#46164=CARTESIAN_POINT('Ctrl Pts',(1.35,-1.64828022648925,-6.94189592925327));
#46165=CARTESIAN_POINT('Ctrl Pts',(1.35,-4.52929005306886,-5.56835021320618));
#46166=CARTESIAN_POINT('Ctrl Pts',(1.35,-6.18684901996756,-3.33902655639443));
#46167=CARTESIAN_POINT('Ctrl Pts',(1.35,-7.00982325588322,-0.7863703147179));
#46168=CARTESIAN_POINT('Ctrl Pts',(1.35,-6.87914556625695,2.33557731371137));
#46169=CARTESIAN_POINT('Ctrl Pts',(1.35,-5.2620311397805,4.71262021528042));
#46170=CARTESIAN_POINT('Ctrl Pts',(1.35,-3.64702851544254,5.88077596934284));
#46171=CARTESIAN_POINT('Ctrl Pts',(1.35,-3.08518962176498,6.18617809038997));
#46172=CARTESIAN_POINT('Ctrl Pts',(1.35,-1.94906065140137,6.66878719035783));
#46173=CARTESIAN_POINT('Ctrl Pts',(1.35,0.477401106171298,7.22296982891625));
#46174=CARTESIAN_POINT('Ctrl Pts',(1.35,4.55752354684712,5.94537013695617));
#46175=CARTESIAN_POINT('Ctrl Pts',(1.35,6.5566669221515,2.80069305436781));
#46176=CARTESIAN_POINT('Ctrl Pts',(1.35,6.86722345981409,0.769068201001234));
#46177=CARTESIAN_POINT('Ctrl Pts',(1.35,6.89384976775196,0.33193295887695));
#46178=CARTESIAN_POINT('Ctrl Pts',(1.35,6.89784386230235,0.172482031811515));
#46179=CARTESIAN_POINT('Ctrl Pts',(0.,6.89784386230235,-0.172482031811513));
#46180=CARTESIAN_POINT('Ctrl Pts',(1.5,6.89784386230235,-0.172482031811513));
#46181=CARTESIAN_POINT('Ctrl Pts',(0.,6.89724474811762,-0.196399670871248));
#46182=CARTESIAN_POINT('Ctrl Pts',(1.5,6.89724474811762,-0.196399670871248));
#46183=CARTESIAN_POINT('Ctrl Pts',(0.,6.89584032941428,-0.244218013275302));
#46184=CARTESIAN_POINT('Ctrl Pts',(1.5,6.89584032941428,-0.244218013275302));
#46185=CARTESIAN_POINT('Ctrl Pts',(0.,6.89311513035763,-0.315894719735146));
#46186=CARTESIAN_POINT('Ctrl Pts',(1.5,6.89311513035763,-0.315894719735146));
#46187=CARTESIAN_POINT('Ctrl Pts',(0.,6.88824437407485,-0.411362046113201));
#46188=CARTESIAN_POINT('Ctrl Pts',(1.5,6.88824437407485,-0.411362046113201));
#46189=CARTESIAN_POINT('Ctrl Pts',(0.,6.88009417679297,-0.530524716562061));
#46190=CARTESIAN_POINT('Ctrl Pts',(1.5,6.88009417679297,-0.530524716562061));
#46191=CARTESIAN_POINT('Ctrl Pts',(0.,6.86988291489663,-0.649509527440788));
#46192=CARTESIAN_POINT('Ctrl Pts',(1.5,6.86988291489663,-0.649509527440788));
#46193=CARTESIAN_POINT('Ctrl Pts',(0.,6.85761207960178,-0.768303743989707));
#46194=CARTESIAN_POINT('Ctrl Pts',(1.5,6.85761207960178,-0.768303743989707));
#46195=CARTESIAN_POINT('Ctrl Pts',(0.,6.84328425996545,-0.886886149588898));
#46196=CARTESIAN_POINT('Ctrl Pts',(1.5,6.84328425996545,-0.886886149588898));
#46197=CARTESIAN_POINT('Ctrl Pts',(0.,6.82690343688202,-1.00522492629022));
#46198=CARTESIAN_POINT('Ctrl Pts',(1.5,6.82690343688202,-1.00522492629022));
#46199=CARTESIAN_POINT('Ctrl Pts',(0.,6.80847475546732,-1.12328081074534));
#46200=CARTESIAN_POINT('Ctrl Pts',(1.5,6.80847475546732,-1.12328081074534));
#46201=CARTESIAN_POINT('Ctrl Pts',(0.,6.78800429750229,-1.24101024985217));
#46202=CARTESIAN_POINT('Ctrl Pts',(1.5,6.78800429750229,-1.24101024985217));
#46203=CARTESIAN_POINT('Ctrl Pts',(0.,6.76549885392698,-1.35836855624314));
#46204=CARTESIAN_POINT('Ctrl Pts',(1.5,6.76549885392698,-1.35836855624314));
#46205=CARTESIAN_POINT('Ctrl Pts',(0.,6.7409656973767,-1.47531306373193));
#46206=CARTESIAN_POINT('Ctrl Pts',(1.5,6.7409656973767,-1.47531306373193));
#46207=CARTESIAN_POINT('Ctrl Pts',(0.,6.71441235475108,-1.59180628284158));
#46208=CARTESIAN_POINT('Ctrl Pts',(1.5,6.71441235475108,-1.59180628284158));
#46209=CARTESIAN_POINT('Ctrl Pts',(0.,6.68584670609465,-1.70781446091543));
#46210=CARTESIAN_POINT('Ctrl Pts',(1.5,6.68584670609465,-1.70781446091543));
#46211=CARTESIAN_POINT('Ctrl Pts',(0.,6.65527708350519,-1.82330614237454));
#46212=CARTESIAN_POINT('Ctrl Pts',(1.5,6.65527708350519,-1.82330614237454));
#46213=CARTESIAN_POINT('Ctrl Pts',(0.,6.62271237007447,-1.93825072906442));
#46214=CARTESIAN_POINT('Ctrl Pts',(1.5,6.62271237007447,-1.93825072906442));
#46215=CARTESIAN_POINT('Ctrl Pts',(0.,6.58816209886438,-2.05261704063842));
#46216=CARTESIAN_POINT('Ctrl Pts',(1.5,6.58816209886438,-2.05261704063842));
#46217=CARTESIAN_POINT('Ctrl Pts',(0.,6.55163655192257,-2.16637187492234));
#46218=CARTESIAN_POINT('Ctrl Pts',(1.5,6.55163655192257,-2.16637187492234));
#46219=CARTESIAN_POINT('Ctrl Pts',(0.,6.5131467128519,-2.2794806466461));
#46220=CARTESIAN_POINT('Ctrl Pts',(1.5,6.5131467128519,-2.2794806466461));
#46221=CARTESIAN_POINT('Ctrl Pts',(0.,6.47270421942094,-2.39190802612683));
#46222=CARTESIAN_POINT('Ctrl Pts',(1.5,6.47270421942094,-2.39190802612683));
#46223=CARTESIAN_POINT('Ctrl Pts',(0.,6.43032131621383,-2.50361857792922));
#46224=CARTESIAN_POINT('Ctrl Pts',(1.5,6.43032131621383,-2.50361857792922));
#46225=CARTESIAN_POINT('Ctrl Pts',(0.,6.38601080731761,-2.61457739952654));
#46226=CARTESIAN_POINT('Ctrl Pts',(1.5,6.38601080731761,-2.61457739952654));
#46227=CARTESIAN_POINT('Ctrl Pts',(0.,6.33978600904486,-2.72475075998758));
#46228=CARTESIAN_POINT('Ctrl Pts',(1.5,6.33978600904486,-2.72475075998758));
#46229=CARTESIAN_POINT('Ctrl Pts',(0.,6.29166076444393,-2.83410583895234));
#46230=CARTESIAN_POINT('Ctrl Pts',(1.5,6.29166076444393,-2.83410583895234));
#46231=CARTESIAN_POINT('Ctrl Pts',(0.,6.24164945784327,-2.94261046564831));
#46232=CARTESIAN_POINT('Ctrl Pts',(1.5,6.24164945784327,-2.94261046564831));
#46233=CARTESIAN_POINT('Ctrl Pts',(0.,6.18976702943031,-3.05023285793724));
#46234=CARTESIAN_POINT('Ctrl Pts',(1.5,6.18976702943031,-3.05023285793724));
#46235=CARTESIAN_POINT('Ctrl Pts',(0.,6.13602898986516,-3.15694136138263));
#46236=CARTESIAN_POINT('Ctrl Pts',(1.5,6.13602898986516,-3.15694136138263));
#46237=CARTESIAN_POINT('Ctrl Pts',(0.,6.0804514349299,-3.26270418832876));
#46238=CARTESIAN_POINT('Ctrl Pts',(1.5,6.0804514349299,-3.26270418832876));
#46239=CARTESIAN_POINT('Ctrl Pts',(0.,6.02305103215795,-3.3674895439004));
#46240=CARTESIAN_POINT('Ctrl Pts',(1.5,6.02305103215795,-3.3674895439004));
#46241=CARTESIAN_POINT('Ctrl Pts',(0.,5.96384500749886,-3.47126575200923));
#46242=CARTESIAN_POINT('Ctrl Pts',(1.5,5.96384500749886,-3.47126575200923));
#46243=CARTESIAN_POINT('Ctrl Pts',(0.,5.90285113201764,-3.57400138137212));
#46244=CARTESIAN_POINT('Ctrl Pts',(1.5,5.90285113201764,-3.57400138137212));
#46245=CARTESIAN_POINT('Ctrl Pts',(0.,5.84008770862799,-3.67566537154608));
#46246=CARTESIAN_POINT('Ctrl Pts',(1.5,5.84008770862799,-3.67566537154608));
#46247=CARTESIAN_POINT('Ctrl Pts',(0.,5.77557355885907,-3.77622715898496));
#46248=CARTESIAN_POINT('Ctrl Pts',(1.5,5.77557355885907,-3.77622715898496));
#46249=CARTESIAN_POINT('Ctrl Pts',(0.,5.70932802034008,-3.87565663572559));
#46250=CARTESIAN_POINT('Ctrl Pts',(1.5,5.70932802034008,-3.87565663572559));
#46251=CARTESIAN_POINT('Ctrl Pts',(0.,5.6413709443175,-3.97392410809942));
#46252=CARTESIAN_POINT('Ctrl Pts',(1.5,5.6413709443175,-3.97392410809942));
#46253=CARTESIAN_POINT('Ctrl Pts',(0.,5.5717226932043,-4.071000255468));
#46254=CARTESIAN_POINT('Ctrl Pts',(1.5,5.5717226932043,-4.071000255468));
#46255=CARTESIAN_POINT('Ctrl Pts',(0.,5.5004041381615,-4.16685608898142));
#46256=CARTESIAN_POINT('Ctrl Pts',(1.5,5.5004041381615,-4.16685608898142));
#46257=CARTESIAN_POINT('Ctrl Pts',(0.,5.42743665671107,-4.26146291035777));
#46258=CARTESIAN_POINT('Ctrl Pts',(1.5,5.42743665671107,-4.26146291035777));
#46259=CARTESIAN_POINT('Ctrl Pts',(0.,5.35284212445925,-4.35479234184529));
#46260=CARTESIAN_POINT('Ctrl Pts',(1.5,5.35284212445925,-4.35479234184529));
#46261=CARTESIAN_POINT('Ctrl Pts',(0.,5.27664290685087,-4.44681635620583));
#46262=CARTESIAN_POINT('Ctrl Pts',(1.5,5.27664290685087,-4.44681635620583));
#46263=CARTESIAN_POINT('Ctrl Pts',(0.,5.19886185095403,-4.53750730672115));
#46264=CARTESIAN_POINT('Ctrl Pts',(1.5,5.19886185095403,-4.53750730672115));
#46265=CARTESIAN_POINT('Ctrl Pts',(0.,5.11952227727487,-4.62683795722317));
#46266=CARTESIAN_POINT('Ctrl Pts',(1.5,5.11952227727487,-4.62683795722317));
#46267=CARTESIAN_POINT('Ctrl Pts',(0.,5.03864797160198,-4.71478151214955));
#46268=CARTESIAN_POINT('Ctrl Pts',(1.5,5.03864797160198,-4.71478151214955));
#46269=CARTESIAN_POINT('Ctrl Pts',(0.,4.95626317819267,-4.80131161496185));
#46270=CARTESIAN_POINT('Ctrl Pts',(1.5,4.95626317819267,-4.80131161496185));
#46271=CARTESIAN_POINT('Ctrl Pts',(0.,4.87239259298808,-4.88640234659096));
#46272=CARTESIAN_POINT('Ctrl Pts',(1.5,4.87239259298808,-4.88640234659096));
#46273=CARTESIAN_POINT('Ctrl Pts',(0.,4.78706135685639,-4.97002822390911));
#46274=CARTESIAN_POINT('Ctrl Pts',(1.5,4.78706135685639,-4.97002822390911));
#46275=CARTESIAN_POINT('Ctrl Pts',(0.,4.70029504886414,-5.05216419822937));
#46276=CARTESIAN_POINT('Ctrl Pts',(1.5,4.70029504886414,-5.05216419822937));
#46277=CARTESIAN_POINT('Ctrl Pts',(0.,4.61211967957449,-5.13278565383202));
#46278=CARTESIAN_POINT('Ctrl Pts',(1.5,4.61211967957449,-5.13278565383202));
#46279=CARTESIAN_POINT('Ctrl Pts',(0.,4.52256168266376,-5.21186841902494));
#46280=CARTESIAN_POINT('Ctrl Pts',(1.5,4.52256168266376,-5.21186841902494));
#46281=CARTESIAN_POINT('Ctrl Pts',(0.,4.43164790656435,-5.28938877723193));
#46282=CARTESIAN_POINT('Ctrl Pts',(1.5,4.43164790656435,-5.28938877723193));
#46283=CARTESIAN_POINT('Ctrl Pts',(0.,4.33940560613361,-5.36532347810974));
#46284=CARTESIAN_POINT('Ctrl Pts',(1.5,4.33940560613361,-5.36532347810974));
#46285=CARTESIAN_POINT('Ctrl Pts',(0.,4.24586243434812,-5.43964974869403));
#46286=CARTESIAN_POINT('Ctrl Pts',(1.5,4.24586243434812,-5.43964974869403));
#46287=CARTESIAN_POINT('Ctrl Pts',(0.,4.1510464340228,-5.51234530457529));
#46288=CARTESIAN_POINT('Ctrl Pts',(1.5,4.1510464340228,-5.51234530457529));
#46289=CARTESIAN_POINT('Ctrl Pts',(0.,4.05498602924829,-5.58338835449849));
#46290=CARTESIAN_POINT('Ctrl Pts',(1.5,4.05498602924829,-5.58338835449849));
#46291=CARTESIAN_POINT('Ctrl Pts',(0.,3.95771001685222,-5.65275760499342));
#46292=CARTESIAN_POINT('Ctrl Pts',(1.5,3.95771001685222,-5.65275760499342));
#46293=CARTESIAN_POINT('Ctrl Pts',(0.,3.85924755788366,-5.72043226503622));
#46294=CARTESIAN_POINT('Ctrl Pts',(1.5,3.85924755788366,-5.72043226503622));
#46295=CARTESIAN_POINT('Ctrl Pts',(0.,3.75962816912048,-5.7863920507423));
#46296=CARTESIAN_POINT('Ctrl Pts',(1.5,3.75962816912048,-5.7863920507423));
#46297=CARTESIAN_POINT('Ctrl Pts',(0.,3.65888171459871,-5.85061719009085));
#46298=CARTESIAN_POINT('Ctrl Pts',(1.5,3.65888171459871,-5.85061719009085));
#46299=CARTESIAN_POINT('Ctrl Pts',(0.,3.55703839636322,-5.91308842921879));
#46300=CARTESIAN_POINT('Ctrl Pts',(1.5,3.55703839636322,-5.91308842921879));
#46301=CARTESIAN_POINT('Ctrl Pts',(0.,3.45412874523946,-5.97378703874717));
#46302=CARTESIAN_POINT('Ctrl Pts',(1.5,3.45412874523946,-5.97378703874717));
#46303=CARTESIAN_POINT('Ctrl Pts',(0.,3.35018361162571,-6.03269482014034));
#46304=CARTESIAN_POINT('Ctrl Pts',(1.5,3.35018361162571,-6.03269482014034));
#46305=CARTESIAN_POINT('Ctrl Pts',(0.,3.2452341563054,-6.08979411209817));
#46306=CARTESIAN_POINT('Ctrl Pts',(1.5,3.2452341563054,-6.08979411209817));
#46307=CARTESIAN_POINT('Ctrl Pts',(0.,3.13931184127879,-6.14506779698192));
#46308=CARTESIAN_POINT('Ctrl Pts',(1.5,3.13931184127879,-6.14506779698192));
#46309=CARTESIAN_POINT('Ctrl Pts',(0.,3.03244842014227,-6.1984993052291));
#46310=CARTESIAN_POINT('Ctrl Pts',(1.5,3.03244842014227,-6.1984993052291));
#46311=CARTESIAN_POINT('Ctrl Pts',(0.,2.92467592848598,-6.25007261980265));
#46312=CARTESIAN_POINT('Ctrl Pts',(1.5,2.92467592848598,-6.25007261980265));
#46313=CARTESIAN_POINT('Ctrl Pts',(0.,2.81602667430891,-6.29977228067469));
#46314=CARTESIAN_POINT('Ctrl Pts',(1.5,2.81602667430891,-6.29977228067469));
#46315=CARTESIAN_POINT('Ctrl Pts',(0.,2.70653322845114,-6.34758338934502));
#46316=CARTESIAN_POINT('Ctrl Pts',(1.5,2.70653322845114,-6.34758338934502));
#46317=CARTESIAN_POINT('Ctrl Pts',(0.,2.59622841504235,-6.39349161339477));
#46318=CARTESIAN_POINT('Ctrl Pts',(1.5,2.59622841504235,-6.39349161339477));
#46319=CARTESIAN_POINT('Ctrl Pts',(0.,2.48514530147603,-6.43748319050759));
#46320=CARTESIAN_POINT('Ctrl Pts',(1.5,2.48514530147603,-6.43748319050759));
#46321=CARTESIAN_POINT('Ctrl Pts',(0.,2.37331718839874,-6.47954493252637));
#46322=CARTESIAN_POINT('Ctrl Pts',(1.5,2.37331718839874,-6.47954493252637));
#46323=CARTESIAN_POINT('Ctrl Pts',(0.,2.26077759971398,-6.51966422954569));
#46324=CARTESIAN_POINT('Ctrl Pts',(1.5,2.26077759971398,-6.51966422954569));
#46325=CARTESIAN_POINT('Ctrl Pts',(0.,2.14756027260008,-6.55782905404073));
#46326=CARTESIAN_POINT('Ctrl Pts',(1.5,2.14756027260008,-6.55782905404073));
#46327=CARTESIAN_POINT('Ctrl Pts',(0.,2.03369914754128,-6.5940279650321));
#46328=CARTESIAN_POINT('Ctrl Pts',(1.5,2.03369914754128,-6.5940279650321));
#46329=CARTESIAN_POINT('Ctrl Pts',(0.,1.91922835801735,-6.6282501110295));
#46330=CARTESIAN_POINT('Ctrl Pts',(1.5,1.91922835801735,-6.6282501110295));
#46331=CARTESIAN_POINT('Ctrl Pts',(0.,1.8041822202052,-6.6604852330121));
#46332=CARTESIAN_POINT('Ctrl Pts',(1.5,1.8041822202052,-6.6604852330121));
#46333=CARTESIAN_POINT('Ctrl Pts',(0.,1.68859522269198,-6.69072366744589));
#46334=CARTESIAN_POINT('Ctrl Pts',(1.5,1.68859522269198,-6.69072366744589));
#46335=CARTESIAN_POINT('Ctrl Pts',(0.,1.57250201619896,-6.71895634933824));
#46336=CARTESIAN_POINT('Ctrl Pts',(1.5,1.57250201619896,-6.71895634933824));
#46337=CARTESIAN_POINT('Ctrl Pts',(0.,1.45593740331553,-6.74517481532982));
#46338=CARTESIAN_POINT('Ctrl Pts',(1.5,1.45593740331553,-6.74517481532982));
#46339=CARTESIAN_POINT('Ctrl Pts',(0.,1.33893632796183,-6.76937120581976));
#46340=CARTESIAN_POINT('Ctrl Pts',(1.5,1.33893632796183,-6.76937120581976));
#46341=CARTESIAN_POINT('Ctrl Pts',(0.,1.22153386486024,-6.79153826712829));
#46342=CARTESIAN_POINT('Ctrl Pts',(1.5,1.22153386486024,-6.79153826712829));
#46343=CARTESIAN_POINT('Ctrl Pts',(0.,1.10376520901503,-6.81166935369773));
#46344=CARTESIAN_POINT('Ctrl Pts',(1.5,1.10376520901503,-6.81166935369773));
#46345=CARTESIAN_POINT('Ctrl Pts',(0.,0.985665665199513,-6.82975843033136));
#46346=CARTESIAN_POINT('Ctrl Pts',(1.5,0.985665665199513,-6.82975843033136));
#46347=CARTESIAN_POINT('Ctrl Pts',(0.,0.867270637450104,-6.84580007447043));
#46348=CARTESIAN_POINT('Ctrl Pts',(1.5,0.867270637450104,-6.84580007447043));
#46349=CARTESIAN_POINT('Ctrl Pts',(0.,0.748615618389539,-6.85978947736425));
#46350=CARTESIAN_POINT('Ctrl Pts',(1.5,0.748615618389539,-6.85978947736425));
#46351=CARTESIAN_POINT('Ctrl Pts',(0.,0.629736178555588,-6.87172244527821));
#46352=CARTESIAN_POINT('Ctrl Pts',(1.5,0.629736178555588,-6.87172244527821));
#46353=CARTESIAN_POINT('Ctrl Pts',(0.,0.510667955734564,-6.8815954007406));
#46354=CARTESIAN_POINT('Ctrl Pts',(1.5,0.510667955734564,-6.8815954007406));
#46355=CARTESIAN_POINT('Ctrl Pts',(0.,0.391446644298975,-6.88940538382764));
#46356=CARTESIAN_POINT('Ctrl Pts',(1.5,0.391446644298975,-6.88940538382764));
#46357=CARTESIAN_POINT('Ctrl Pts',(0.,0.272107984548754,-6.8951500534872));
#46358=CARTESIAN_POINT('Ctrl Pts',(1.5,0.272107984548754,-6.8951500534872));
#46359=CARTESIAN_POINT('Ctrl Pts',(0.,0.152687751971164,-6.89882768779677));
#46360=CARTESIAN_POINT('Ctrl Pts',(1.5,0.152687751971164,-6.89882768779677));
#46361=CARTESIAN_POINT('Ctrl Pts',(0.,0.0332217465029873,-6.90043718426009));
#46362=CARTESIAN_POINT('Ctrl Pts',(1.5,0.0332217465029873,-6.90043718426009));
#46363=CARTESIAN_POINT('Ctrl Pts',(0.,-0.0862542182058646,-6.89997806014264));
#46364=CARTESIAN_POINT('Ctrl Pts',(1.5,-0.0862542182058646,-6.89997806014264));
#46365=CARTESIAN_POINT('Ctrl Pts',(0.,-0.205704325527785,-6.8974504528457));
#46366=CARTESIAN_POINT('Ctrl Pts',(1.5,-0.205704325527785,-6.8974504528457));
#46367=CARTESIAN_POINT('Ctrl Pts',(0.,-0.325092766592762,-6.89285512031913));
#46368=CARTESIAN_POINT('Ctrl Pts',(1.5,-0.325092766592762,-6.89285512031913));
#46369=CARTESIAN_POINT('Ctrl Pts',(0.,-0.444383751009717,-6.88619344038296));
#46370=CARTESIAN_POINT('Ctrl Pts',(1.5,-0.444383751009717,-6.88619344038296));
#46371=CARTESIAN_POINT('Ctrl Pts',(0.,-0.563541517589008,-6.87746741008788));
#46372=CARTESIAN_POINT('Ctrl Pts',(1.5,-0.563541517589008,-6.87746741008788));
#46373=CARTESIAN_POINT('Ctrl Pts',(0.,-0.682530345066741,-6.86667964511437));
#46374=CARTESIAN_POINT('Ctrl Pts',(1.5,-0.682530345066741,-6.86667964511437));
#46375=CARTESIAN_POINT('Ctrl Pts',(0.,-0.801314562831502,-6.85383337921045));
#46376=CARTESIAN_POINT('Ctrl Pts',(1.5,-0.801314562831502,-6.85383337921045));
#46377=CARTESIAN_POINT('Ctrl Pts',(0.,-0.919858561654232,-6.83893246366781));
#46378=CARTESIAN_POINT('Ctrl Pts',(1.5,-0.919858561654232,-6.83893246366781));
#46379=CARTESIAN_POINT('Ctrl Pts',(0.,-1.03812680431107,-6.82198136572201));
#46380=CARTESIAN_POINT('Ctrl Pts',(1.5,-1.03812680431107,-6.82198136572201));
#46381=CARTESIAN_POINT('Ctrl Pts',(0.,-1.15608383621068,-6.80298516699082));
#46382=CARTESIAN_POINT('Ctrl Pts',(1.5,-1.15608383621068,-6.80298516699082));
#46383=CARTESIAN_POINT('Ctrl Pts',(0.,-1.27369429602679,-6.78194956195138));
#46384=CARTESIAN_POINT('Ctrl Pts',(1.5,-1.27369429602679,-6.78194956195138));
#46385=CARTESIAN_POINT('Ctrl Pts',(0.,-1.39092292633656,-6.7588808564554));
#46386=CARTESIAN_POINT('Ctrl Pts',(1.5,-1.39092292633656,-6.7588808564554));
#46387=CARTESIAN_POINT('Ctrl Pts',(0.,-1.50773458426541,-6.73378596628269));
#46388=CARTESIAN_POINT('Ctrl Pts',(1.5,-1.50773458426541,-6.73378596628269));
#46389=CARTESIAN_POINT('Ctrl Pts',(0.,-1.62409425193172,-6.70667241462751));
#46390=CARTESIAN_POINT('Ctrl Pts',(1.5,-1.62409425193172,-6.70667241462751));
#46391=CARTESIAN_POINT('Ctrl Pts',(0.,-1.7399670468992,-6.67754832962271));
#46392=CARTESIAN_POINT('Ctrl Pts',(1.5,-1.7399670468992,-6.67754832962271));
#46393=CARTESIAN_POINT('Ctrl Pts',(0.,-1.85531823263776,-6.64642244190193));
#46394=CARTESIAN_POINT('Ctrl Pts',(1.5,-1.85531823263776,-6.64642244190193));
#46395=CARTESIAN_POINT('Ctrl Pts',(0.,-1.97011322899335,-6.61330408219923));
#46396=CARTESIAN_POINT('Ctrl Pts',(1.5,-1.97011322899335,-6.61330408219923));
#46397=CARTESIAN_POINT('Ctrl Pts',(0.,-2.08431762266778,-6.57820317898646));
#46398=CARTESIAN_POINT('Ctrl Pts',(1.5,-2.08431762266778,-6.57820317898646));
#46399=CARTESIAN_POINT('Ctrl Pts',(0.,-2.19789717740688,-6.54113025506627));
#46400=CARTESIAN_POINT('Ctrl Pts',(1.5,-2.19789717740688,-6.54113025506627));
#46401=CARTESIAN_POINT('Ctrl Pts',(0.,-2.31081784419971,-6.5020964242025));
#46402=CARTESIAN_POINT('Ctrl Pts',(1.5,-2.31081784419971,-6.5020964242025));
#46403=CARTESIAN_POINT('Ctrl Pts',(0.,-2.42304577148957,-6.4611133877874));
#46404=CARTESIAN_POINT('Ctrl Pts',(1.5,-2.42304577148957,-6.4611133877874));
#46405=CARTESIAN_POINT('Ctrl Pts',(0.,-2.53454731539729,-6.41819343154569));
#46406=CARTESIAN_POINT('Ctrl Pts',(1.5,-2.53454731539729,-6.41819343154569));
#46407=CARTESIAN_POINT('Ctrl Pts',(0.,-2.64528904995755,-6.37334942227507));
#46408=CARTESIAN_POINT('Ctrl Pts',(1.5,-2.64528904995755,-6.37334942227507));
#46409=CARTESIAN_POINT('Ctrl Pts',(0.,-2.75523777697425,-6.32659480357096));
#46410=CARTESIAN_POINT('Ctrl Pts',(1.5,-2.75523777697425,-6.32659480357096));
#46411=CARTESIAN_POINT('Ctrl Pts',(0.,-2.86436053589027,-6.27794359158745));
#46412=CARTESIAN_POINT('Ctrl Pts',(1.5,-2.86436053589027,-6.27794359158745));
#46413=CARTESIAN_POINT('Ctrl Pts',(0.,-2.97262461367192,-6.22741037083388));
#46414=CARTESIAN_POINT('Ctrl Pts',(1.5,-2.97262461367192,-6.22741037083388));
#46415=CARTESIAN_POINT('Ctrl Pts',(0.,-3.07999755470908,-6.17501029000702));
#46416=CARTESIAN_POINT('Ctrl Pts',(1.5,-3.07999755470908,-6.17501029000702));
#46417=CARTESIAN_POINT('Ctrl Pts',(0.,-3.18644717073111,-6.12075905785837));
#46418=CARTESIAN_POINT('Ctrl Pts',(1.5,-3.18644717073111,-6.12075905785837));
#46419=CARTESIAN_POINT('Ctrl Pts',(0.,-3.29194155025575,-6.06467293808302));
#46420=CARTESIAN_POINT('Ctrl Pts',(1.5,-3.29194155025575,-6.06467293808302));
#46421=CARTESIAN_POINT('Ctrl Pts',(0.,-3.39644906805528,-6.00676874424304));
#46422=CARTESIAN_POINT('Ctrl Pts',(1.5,-3.39644906805528,-6.00676874424304));
#46423=CARTESIAN_POINT('Ctrl Pts',(0.,-3.49993839464067,-5.94706383472536));
#46424=CARTESIAN_POINT('Ctrl Pts',(1.5,-3.49993839464067,-5.94706383472536));
#46425=CARTESIAN_POINT('Ctrl Pts',(0.,-3.60237850576418,-5.88557610773356));
#46426=CARTESIAN_POINT('Ctrl Pts',(1.5,-3.60237850576418,-5.88557610773356));
#46427=CARTESIAN_POINT('Ctrl Pts',(0.,-3.70373869194093,-5.82232399631353));
#46428=CARTESIAN_POINT('Ctrl Pts',(1.5,-3.70373869194093,-5.82232399631353));
#46429=CARTESIAN_POINT('Ctrl Pts',(0.,-3.80398856742054,-5.75732646244435));
#46430=CARTESIAN_POINT('Ctrl Pts',(1.5,-3.80398856742054,-5.75732646244435));
#46431=CARTESIAN_POINT('Ctrl Pts',(0.,-3.90309807917881,-5.69060299116233));
#46432=CARTESIAN_POINT('Ctrl Pts',(1.5,-3.90309807917881,-5.69060299116233));
#46433=CARTESIAN_POINT('Ctrl Pts',(0.,-4.00103751593049,-5.62217358471744));
#46434=CARTESIAN_POINT('Ctrl Pts',(1.5,-4.00103751593049,-5.62217358471744));
#46435=CARTESIAN_POINT('Ctrl Pts',(0.,-4.09777751716309,-5.55205875676251));
#46436=CARTESIAN_POINT('Ctrl Pts',(1.5,-4.09777751716309,-5.55205875676251));
#46437=CARTESIAN_POINT('Ctrl Pts',(0.,-4.19328908219274,-5.48027952657387));
#46438=CARTESIAN_POINT('Ctrl Pts',(1.5,-4.19328908219274,-5.48027952657387));
#46439=CARTESIAN_POINT('Ctrl Pts',(0.,-4.28754357859123,-5.4068574123888));
#46440=CARTESIAN_POINT('Ctrl Pts',(1.5,-4.28754357859123,-5.4068574123888));
#46441=CARTESIAN_POINT('Ctrl Pts',(0.,-4.38051275063608,-5.33181442477391));
#46442=CARTESIAN_POINT('Ctrl Pts',(1.5,-4.38051275063608,-5.33181442477391));
#46443=CARTESIAN_POINT('Ctrl Pts',(0.,-4.47216872778419,-5.25517306002452));
#46444=CARTESIAN_POINT('Ctrl Pts',(1.5,-4.47216872778419,-5.25517306002452));
#46445=CARTESIAN_POINT('Ctrl Pts',(0.,-4.56248403316946,-5.17695629359431));
#46446=CARTESIAN_POINT('Ctrl Pts',(1.5,-4.56248403316946,-5.17695629359431));
#46447=CARTESIAN_POINT('Ctrl Pts',(0.,-4.65143159212514,-5.09718757355493));
#46448=CARTESIAN_POINT('Ctrl Pts',(1.5,-4.65143159212514,-5.09718757355493));
#46449=CARTESIAN_POINT('Ctrl Pts',(0.,-4.7389847400031,-5.01589081322949));
#46450=CARTESIAN_POINT('Ctrl Pts',(1.5,-4.7389847400031,-5.01589081322949));
#46451=CARTESIAN_POINT('Ctrl Pts',(0.,-4.82511723001895,-4.93309038385534));
#46452=CARTESIAN_POINT('Ctrl Pts',(1.5,-4.82511723001895,-4.93309038385534));
#46453=CARTESIAN_POINT('Ctrl Pts',(0.,-4.9098032411231,-4.84881110727519));
#46454=CARTESIAN_POINT('Ctrl Pts',(1.5,-4.9098032411231,-4.84881110727519));
#46455=CARTESIAN_POINT('Ctrl Pts',(0.,-4.99301738589862,-4.76307824865675));
#46456=CARTESIAN_POINT('Ctrl Pts',(1.5,-4.99301738589862,-4.76307824865675));
#46457=CARTESIAN_POINT('Ctrl Pts',(0.,-5.07473471848603,-4.67591750924002));
#46458=CARTESIAN_POINT('Ctrl Pts',(1.5,-5.07473471848603,-4.67591750924002));
#46459=CARTESIAN_POINT('Ctrl Pts',(0.,-5.1549307417364,-4.5873550183222));
#46460=CARTESIAN_POINT('Ctrl Pts',(1.5,-5.1549307417364,-4.5873550183222));
#46461=CARTESIAN_POINT('Ctrl Pts',(0.,-5.23358141439273,-4.49741732526974));
#46462=CARTESIAN_POINT('Ctrl Pts',(1.5,-5.23358141439273,-4.49741732526974));
#46463=CARTESIAN_POINT('Ctrl Pts',(0.,-5.31066315829954,-4.40613139155633));
#46464=CARTESIAN_POINT('Ctrl Pts',(1.5,-5.31066315829954,-4.40613139155633));
#46465=CARTESIAN_POINT('Ctrl Pts',(0.,-5.38615286564164,-4.31352458282688));
#46466=CARTESIAN_POINT('Ctrl Pts',(1.5,-5.38615286564164,-4.31352458282688));
#46467=CARTESIAN_POINT('Ctrl Pts',(0.,-5.46002790621214,-4.21962466098661));
#46468=CARTESIAN_POINT('Ctrl Pts',(1.5,-5.46002790621214,-4.21962466098661));
#46469=CARTESIAN_POINT('Ctrl Pts',(0.,-5.53226613384586,-4.12445977559767));
#46470=CARTESIAN_POINT('Ctrl Pts',(1.5,-5.53226613384586,-4.12445977559767));
#46471=CARTESIAN_POINT('Ctrl Pts',(0.,-5.60284589288301,-4.02805845530006));
#46472=CARTESIAN_POINT('Ctrl Pts',(1.5,-5.60284589288301,-4.02805845530006));
#46473=CARTESIAN_POINT('Ctrl Pts',(0.,-5.67174602466349,-3.93044959925604));
#46474=CARTESIAN_POINT('Ctrl Pts',(1.5,-5.67174602466349,-3.93044959925604));
#46475=CARTESIAN_POINT('Ctrl Pts',(0.,-5.73894587405215,-3.8316624686178));
#46476=CARTESIAN_POINT('Ctrl Pts',(1.5,-5.73894587405215,-3.8316624686178));
#46477=CARTESIAN_POINT('Ctrl Pts',(0.,-5.80442529599575,-3.731726678018));
#46478=CARTESIAN_POINT('Ctrl Pts',(1.5,-5.80442529599575,-3.731726678018));
#46479=CARTESIAN_POINT('Ctrl Pts',(0.,-5.86816466118834,-3.63067218644238));
#46480=CARTESIAN_POINT('Ctrl Pts',(1.5,-5.86816466118834,-3.63067218644238));
#46481=CARTESIAN_POINT('Ctrl Pts',(0.,-5.93014486176895,-3.52852928812396));
#46482=CARTESIAN_POINT('Ctrl Pts',(1.5,-5.93014486176895,-3.52852928812396));
#46483=CARTESIAN_POINT('Ctrl Pts',(0.,-5.99034731705189,-3.42532860345791));
#46484=CARTESIAN_POINT('Ctrl Pts',(1.5,-5.99034731705189,-3.42532860345791));
#46485=CARTESIAN_POINT('Ctrl Pts',(0.,-6.04875397928989,-3.32110106993708));
#46486=CARTESIAN_POINT('Ctrl Pts',(1.5,-6.04875397928989,-3.32110106993708));
#46487=CARTESIAN_POINT('Ctrl Pts',(0.,-6.10534733947052,-3.2158779331071));
#46488=CARTESIAN_POINT('Ctrl Pts',(1.5,-6.10534733947052,-3.2158779331071));
#46489=CARTESIAN_POINT('Ctrl Pts',(0.,-6.16011043217119,-3.10969073698348));
#46490=CARTESIAN_POINT('Ctrl Pts',(1.5,-6.16011043217119,-3.10969073698348));
#46491=CARTESIAN_POINT('Ctrl Pts',(0.,-6.21302684044837,-3.00257131448723));
#46492=CARTESIAN_POINT('Ctrl Pts',(1.5,-6.21302684044837,-3.00257131448723));
#46493=CARTESIAN_POINT('Ctrl Pts',(0.,-6.26408070076069,-2.89455177789849));
#46494=CARTESIAN_POINT('Ctrl Pts',(1.5,-6.26408070076069,-2.89455177789849));
#46495=CARTESIAN_POINT('Ctrl Pts',(0.,-6.31325670792693,-2.78566450932763));
#46496=CARTESIAN_POINT('Ctrl Pts',(1.5,-6.31325670792693,-2.78566450932763));
#46497=CARTESIAN_POINT('Ctrl Pts',(0.,-6.36054012011854,-2.67594215120311));
#46498=CARTESIAN_POINT('Ctrl Pts',(1.5,-6.36054012011854,-2.67594215120311));
#46499=CARTESIAN_POINT('Ctrl Pts',(0.,-6.40591676286809,-2.56541759630458));
#46500=CARTESIAN_POINT('Ctrl Pts',(1.5,-6.40591676286809,-2.56541759630458));
#46501=CARTESIAN_POINT('Ctrl Pts',(0.,-6.44937303311288,-2.45412397781148));
#46502=CARTESIAN_POINT('Ctrl Pts',(1.5,-6.44937303311288,-2.45412397781148));
#46503=CARTESIAN_POINT('Ctrl Pts',(0.,-6.49089590327433,-2.34209465936682));
#46504=CARTESIAN_POINT('Ctrl Pts',(1.5,-6.49089590327433,-2.34209465936682));
#46505=CARTESIAN_POINT('Ctrl Pts',(0.,-6.53047292537357,-2.22936322515532));
#46506=CARTESIAN_POINT('Ctrl Pts',(1.5,-6.53047292537357,-2.22936322515532));
#46507=CARTESIAN_POINT('Ctrl Pts',(0.,-6.56809223518283,-2.11596346999528));
#46508=CARTESIAN_POINT('Ctrl Pts',(1.5,-6.56809223518283,-2.11596346999528));
#46509=CARTESIAN_POINT('Ctrl Pts',(0.,-6.60374255535696,-2.00192938906232));
#46510=CARTESIAN_POINT('Ctrl Pts',(1.5,-6.60374255535696,-2.00192938906232));
#46511=CARTESIAN_POINT('Ctrl Pts',(0.,-6.63741319860151,-1.8872951676257));
#46512=CARTESIAN_POINT('Ctrl Pts',(1.5,-6.63741319860151,-1.8872951676257));
#46513=CARTESIAN_POINT('Ctrl Pts',(0.,-6.66909407087783,-1.77209517079654));
#46514=CARTESIAN_POINT('Ctrl Pts',(1.5,-6.66909407087783,-1.77209517079654));
#46515=CARTESIAN_POINT('Ctrl Pts',(0.,-6.69877567464511,-1.65636393328722));
#46516=CARTESIAN_POINT('Ctrl Pts',(1.5,-6.69877567464511,-1.65636393328722));
#46517=CARTESIAN_POINT('Ctrl Pts',(0.,-6.72644911213981,-1.54013614918151));
#46518=CARTESIAN_POINT('Ctrl Pts',(1.5,-6.72644911213981,-1.54013614918151));
#46519=CARTESIAN_POINT('Ctrl Pts',(0.,-6.75210608760682,-1.42344666142604));
#46520=CARTESIAN_POINT('Ctrl Pts',(1.5,-6.75210608760682,-1.42344666142604));
#46521=CARTESIAN_POINT('Ctrl Pts',(0.,-6.77573890956821,-1.30633045133105));
#46522=CARTESIAN_POINT('Ctrl Pts',(1.5,-6.77573890956821,-1.30633045133105));
#46523=CARTESIAN_POINT('Ctrl Pts',(0.,-6.79734049312989,-1.18882262807986));
#46524=CARTESIAN_POINT('Ctrl Pts',(1.5,-6.79734049312989,-1.18882262807986));
#46525=CARTESIAN_POINT('Ctrl Pts',(0.,-6.81690436232613,-1.07095841824634));
#46526=CARTESIAN_POINT('Ctrl Pts',(1.5,-6.81690436232613,-1.07095841824634));
#46527=CARTESIAN_POINT('Ctrl Pts',(0.,-6.83442465250206,-0.952773155319746));
#46528=CARTESIAN_POINT('Ctrl Pts',(1.5,-6.83442465250206,-0.952773155319746));
#46529=CARTESIAN_POINT('Ctrl Pts',(0.,-6.84989611162797,-0.834302269042729));
#46530=CARTESIAN_POINT('Ctrl Pts',(1.5,-6.84989611162797,-0.834302269042729));
#46531=CARTESIAN_POINT('Ctrl Pts',(0.,-6.86331410165185,-0.715581274755232));
#46532=CARTESIAN_POINT('Ctrl Pts',(1.5,-6.86331410165185,-0.715581274755232));
#46533=CARTESIAN_POINT('Ctrl Pts',(0.,-6.87467459989036,-0.596645762743843));
#46534=CARTESIAN_POINT('Ctrl Pts',(1.5,-6.87467459989036,-0.596645762743843));
#46535=CARTESIAN_POINT('Ctrl Pts',(0.,-6.88397420045809,-0.477531387595776));
#46536=CARTESIAN_POINT('Ctrl Pts',(1.5,-6.88397420045809,-0.477531387595776));
#46537=CARTESIAN_POINT('Ctrl Pts',(0.,-6.89121011573542,-0.358273857556864));
#46538=CARTESIAN_POINT('Ctrl Pts',(1.5,-6.89121011573542,-0.358273857556864));
#46539=CARTESIAN_POINT('Ctrl Pts',(0.,-6.89638017675603,-0.238908923795811));
#46540=CARTESIAN_POINT('Ctrl Pts',(1.5,-6.89638017675603,-0.238908923795811));
#46541=CARTESIAN_POINT('Ctrl Pts',(0.,-6.89948283363306,-0.119472369671119));
#46542=CARTESIAN_POINT('Ctrl Pts',(1.5,-6.89948283363306,-0.119472369671119));
#46543=CARTESIAN_POINT('Ctrl Pts',(0.,-6.90051715602375,-6.41517004448811E-14));
#46544=CARTESIAN_POINT('Ctrl Pts',(1.5,-6.90051715602375,-6.41517004448811E-14));
#46545=CARTESIAN_POINT('Ctrl Pts',(0.,-6.89948283363311,0.119472369671016));
#46546=CARTESIAN_POINT('Ctrl Pts',(1.5,-6.89948283363311,0.119472369671016));
#46547=CARTESIAN_POINT('Ctrl Pts',(0.,-6.8963801767561,0.238908923795769));
#46548=CARTESIAN_POINT('Ctrl Pts',(1.5,-6.8963801767561,0.238908923795769));
#46549=CARTESIAN_POINT('Ctrl Pts',(0.,-6.89121011573547,0.358273857556871));
#46550=CARTESIAN_POINT('Ctrl Pts',(1.5,-6.89121011573547,0.358273857556871));
#46551=CARTESIAN_POINT('Ctrl Pts',(0.,-6.88397420045813,0.477531387595768));
#46552=CARTESIAN_POINT('Ctrl Pts',(1.5,-6.88397420045813,0.477531387595768));
#46553=CARTESIAN_POINT('Ctrl Pts',(0.,-6.87467459989038,0.596645762743742));
#46554=CARTESIAN_POINT('Ctrl Pts',(1.5,-6.87467459989038,0.596645762743742));
#46555=CARTESIAN_POINT('Ctrl Pts',(0.,-6.8633141016518,0.715581274754981));
#46556=CARTESIAN_POINT('Ctrl Pts',(1.5,-6.8633141016518,0.715581274754981));
#46557=CARTESIAN_POINT('Ctrl Pts',(0.,-6.84989611162784,0.834302269042349));
#46558=CARTESIAN_POINT('Ctrl Pts',(1.5,-6.84989611162784,0.834302269042349));
#46559=CARTESIAN_POINT('Ctrl Pts',(0.,-6.83442465250195,0.952773155319338));
#46560=CARTESIAN_POINT('Ctrl Pts',(1.5,-6.83442465250195,0.952773155319338));
#46561=CARTESIAN_POINT('Ctrl Pts',(0.,-6.81690436232608,1.07095841824604));
#46562=CARTESIAN_POINT('Ctrl Pts',(1.5,-6.81690436232608,1.07095841824604));
#46563=CARTESIAN_POINT('Ctrl Pts',(0.,-6.79734049312992,1.18882262807975));
#46564=CARTESIAN_POINT('Ctrl Pts',(1.5,-6.79734049312992,1.18882262807975));
#46565=CARTESIAN_POINT('Ctrl Pts',(0.,-6.77573890956825,1.30633045133112));
#46566=CARTESIAN_POINT('Ctrl Pts',(1.5,-6.77573890956825,1.30633045133112));
#46567=CARTESIAN_POINT('Ctrl Pts',(0.,-6.75210608760686,1.42344666142619));
#46568=CARTESIAN_POINT('Ctrl Pts',(1.5,-6.75210608760686,1.42344666142619));
#46569=CARTESIAN_POINT('Ctrl Pts',(0.,-6.72644911213985,1.54013614918161));
#46570=CARTESIAN_POINT('Ctrl Pts',(1.5,-6.72644911213985,1.54013614918161));
#46571=CARTESIAN_POINT('Ctrl Pts',(0.,-6.69877567464515,1.6563639332872));
#46572=CARTESIAN_POINT('Ctrl Pts',(1.5,-6.69877567464515,1.6563639332872));
#46573=CARTESIAN_POINT('Ctrl Pts',(0.,-6.66909407087785,1.77209517079641));
#46574=CARTESIAN_POINT('Ctrl Pts',(1.5,-6.66909407087785,1.77209517079641));
#46575=CARTESIAN_POINT('Ctrl Pts',(0.,-6.63741319860154,1.88729516762555));
#46576=CARTESIAN_POINT('Ctrl Pts',(1.5,-6.63741319860154,1.88729516762555));
#46577=CARTESIAN_POINT('Ctrl Pts',(0.,-6.603742555357,2.0019293890622));
#46578=CARTESIAN_POINT('Ctrl Pts',(1.5,-6.603742555357,2.0019293890622));
#46579=CARTESIAN_POINT('Ctrl Pts',(0.,-6.56809223518289,2.11596346999519));
#46580=CARTESIAN_POINT('Ctrl Pts',(1.5,-6.56809223518289,2.11596346999519));
#46581=CARTESIAN_POINT('Ctrl Pts',(0.,-6.53047292537362,2.22936322515524));
#46582=CARTESIAN_POINT('Ctrl Pts',(1.5,-6.53047292537362,2.22936322515524));
#46583=CARTESIAN_POINT('Ctrl Pts',(0.,-6.49089590327437,2.34209465936671));
#46584=CARTESIAN_POINT('Ctrl Pts',(1.5,-6.49089590327437,2.34209465936671));
#46585=CARTESIAN_POINT('Ctrl Pts',(0.,-6.44937303311289,2.45412397781135));
#46586=CARTESIAN_POINT('Ctrl Pts',(1.5,-6.44937303311289,2.45412397781135));
#46587=CARTESIAN_POINT('Ctrl Pts',(0.,-6.40591676286813,2.56541759630447));
#46588=CARTESIAN_POINT('Ctrl Pts',(1.5,-6.40591676286813,2.56541759630447));
#46589=CARTESIAN_POINT('Ctrl Pts',(0.,-6.3605401201186,2.67594215120304));
#46590=CARTESIAN_POINT('Ctrl Pts',(1.5,-6.3605401201186,2.67594215120304));
#46591=CARTESIAN_POINT('Ctrl Pts',(0.,-6.31325670792698,2.78566450932757));
#46592=CARTESIAN_POINT('Ctrl Pts',(1.5,-6.31325670792698,2.78566450932757));
#46593=CARTESIAN_POINT('Ctrl Pts',(0.,-6.26408070076075,2.8945517778984));
#46594=CARTESIAN_POINT('Ctrl Pts',(1.5,-6.26408070076075,2.8945517778984));
#46595=CARTESIAN_POINT('Ctrl Pts',(0.,-6.2130268404484,3.00257131448706));
#46596=CARTESIAN_POINT('Ctrl Pts',(1.5,-6.2130268404484,3.00257131448706));
#46597=CARTESIAN_POINT('Ctrl Pts',(0.,-6.16011043217123,3.10969073698327));
#46598=CARTESIAN_POINT('Ctrl Pts',(1.5,-6.16011043217123,3.10969073698327));
#46599=CARTESIAN_POINT('Ctrl Pts',(0.,-6.10534733947057,3.2158779331069));
#46600=CARTESIAN_POINT('Ctrl Pts',(1.5,-6.10534733947057,3.2158779331069));
#46601=CARTESIAN_POINT('Ctrl Pts',(0.,-6.04875397928998,3.32110106993695));
#46602=CARTESIAN_POINT('Ctrl Pts',(1.5,-6.04875397928998,3.32110106993695));
#46603=CARTESIAN_POINT('Ctrl Pts',(0.,-5.99034731705195,3.42532860345784));
#46604=CARTESIAN_POINT('Ctrl Pts',(1.5,-5.99034731705195,3.42532860345784));
#46605=CARTESIAN_POINT('Ctrl Pts',(0.,-5.93014486176895,3.52852928812384));
#46606=CARTESIAN_POINT('Ctrl Pts',(1.5,-5.93014486176895,3.52852928812384));
#46607=CARTESIAN_POINT('Ctrl Pts',(0.,-5.86816466118828,3.63067218644218));
#46608=CARTESIAN_POINT('Ctrl Pts',(1.5,-5.86816466118828,3.63067218644218));
#46609=CARTESIAN_POINT('Ctrl Pts',(0.,-5.8044252959957,3.73172667801772));
#46610=CARTESIAN_POINT('Ctrl Pts',(1.5,-5.8044252959957,3.73172667801772));
#46611=CARTESIAN_POINT('Ctrl Pts',(0.,-5.73894587405215,3.83166246861755));
#46612=CARTESIAN_POINT('Ctrl Pts',(1.5,-5.73894587405215,3.83166246861755));
#46613=CARTESIAN_POINT('Ctrl Pts',(0.,-5.67174602466356,3.93044959925594));
#46614=CARTESIAN_POINT('Ctrl Pts',(1.5,-5.67174602466356,3.93044959925594));
#46615=CARTESIAN_POINT('Ctrl Pts',(0.,-5.60284589288313,4.02805845530014));
#46616=CARTESIAN_POINT('Ctrl Pts',(1.5,-5.60284589288313,4.02805845530014));
#46617=CARTESIAN_POINT('Ctrl Pts',(0.,-5.53226613384595,4.12445977559781));
#46618=CARTESIAN_POINT('Ctrl Pts',(1.5,-5.53226613384595,4.12445977559781));
#46619=CARTESIAN_POINT('Ctrl Pts',(0.,-5.46002790621221,4.2196246609867));
#46620=CARTESIAN_POINT('Ctrl Pts',(1.5,-5.46002790621221,4.2196246609867));
#46621=CARTESIAN_POINT('Ctrl Pts',(0.,-5.38615286564171,4.3135245828269));
#46622=CARTESIAN_POINT('Ctrl Pts',(1.5,-5.38615286564171,4.3135245828269));
#46623=CARTESIAN_POINT('Ctrl Pts',(0.,-5.31066315829961,4.40613139155624));
#46624=CARTESIAN_POINT('Ctrl Pts',(1.5,-5.31066315829961,4.40613139155624));
#46625=CARTESIAN_POINT('Ctrl Pts',(0.,-5.2335814143928,4.49741732526956));
#46626=CARTESIAN_POINT('Ctrl Pts',(1.5,-5.2335814143928,4.49741732526956));
#46627=CARTESIAN_POINT('Ctrl Pts',(0.,-5.15493074173648,4.58735501832194));
#46628=CARTESIAN_POINT('Ctrl Pts',(1.5,-5.15493074173648,4.58735501832194));
#46629=CARTESIAN_POINT('Ctrl Pts',(0.,-5.0747347184861,4.67591750923974));
#46630=CARTESIAN_POINT('Ctrl Pts',(1.5,-5.0747347184861,4.67591750923974));
#46631=CARTESIAN_POINT('Ctrl Pts',(0.,-4.9930173858987,4.76307824865654));
#46632=CARTESIAN_POINT('Ctrl Pts',(1.5,-4.9930173858987,4.76307824865654));
#46633=CARTESIAN_POINT('Ctrl Pts',(0.,-4.90980324112317,4.84881110727509));
#46634=CARTESIAN_POINT('Ctrl Pts',(1.5,-4.90980324112317,4.84881110727509));
#46635=CARTESIAN_POINT('Ctrl Pts',(0.,-4.82511723001905,4.93309038385543));
#46636=CARTESIAN_POINT('Ctrl Pts',(1.5,-4.82511723001905,4.93309038385543));
#46637=CARTESIAN_POINT('Ctrl Pts',(0.,-4.73898474000325,5.01589081322972));
#46638=CARTESIAN_POINT('Ctrl Pts',(1.5,-4.73898474000325,5.01589081322972));
#46639=CARTESIAN_POINT('Ctrl Pts',(0.,-4.6514315921253,5.09718757355513));
#46640=CARTESIAN_POINT('Ctrl Pts',(1.5,-4.6514315921253,5.09718757355513));
#46641=CARTESIAN_POINT('Ctrl Pts',(0.,-4.5624840331696,5.17695629359438));
#46642=CARTESIAN_POINT('Ctrl Pts',(1.5,-4.5624840331696,5.17695629359438));
#46643=CARTESIAN_POINT('Ctrl Pts',(0.,-4.47216872778426,5.25517306002443));
#46644=CARTESIAN_POINT('Ctrl Pts',(1.5,-4.47216872778426,5.25517306002443));
#46645=CARTESIAN_POINT('Ctrl Pts',(0.,-4.38051275063613,5.33181442477374));
#46646=CARTESIAN_POINT('Ctrl Pts',(1.5,-4.38051275063613,5.33181442477374));
#46647=CARTESIAN_POINT('Ctrl Pts',(0.,-4.28754357859128,5.40685741238864));
#46648=CARTESIAN_POINT('Ctrl Pts',(1.5,-4.28754357859128,5.40685741238864));
#46649=CARTESIAN_POINT('Ctrl Pts',(0.,-4.19328908219282,5.48027952657378));
#46650=CARTESIAN_POINT('Ctrl Pts',(1.5,-4.19328908219282,5.48027952657378));
#46651=CARTESIAN_POINT('Ctrl Pts',(0.,-4.0977775171632,5.55205875676246));
#46652=CARTESIAN_POINT('Ctrl Pts',(1.5,-4.0977775171632,5.55205875676246));
#46653=CARTESIAN_POINT('Ctrl Pts',(0.,-4.0010375159306,5.62217358471739));
#46654=CARTESIAN_POINT('Ctrl Pts',(1.5,-4.0010375159306,5.62217358471739));
#46655=CARTESIAN_POINT('Ctrl Pts',(0.,-3.90309807917886,5.69060299116221));
#46656=CARTESIAN_POINT('Ctrl Pts',(1.5,-3.90309807917886,5.69060299116221));
#46657=CARTESIAN_POINT('Ctrl Pts',(0.,-3.80398856742053,5.7573264624442));
#46658=CARTESIAN_POINT('Ctrl Pts',(1.5,-3.80398856742053,5.7573264624442));
#46659=CARTESIAN_POINT('Ctrl Pts',(0.,-3.70373869194093,5.82232399631334));
#46660=CARTESIAN_POINT('Ctrl Pts',(1.5,-3.70373869194093,5.82232399631334));
#46661=CARTESIAN_POINT('Ctrl Pts',(0.,-3.60237850576421,5.88557610773341));
#46662=CARTESIAN_POINT('Ctrl Pts',(1.5,-3.60237850576421,5.88557610773341));
#46663=CARTESIAN_POINT('Ctrl Pts',(0.,-3.49993839464077,5.9470638347253));
#46664=CARTESIAN_POINT('Ctrl Pts',(1.5,-3.49993839464077,5.9470638347253));
#46665=CARTESIAN_POINT('Ctrl Pts',(0.,-3.39644906805545,6.00676874424307));
#46666=CARTESIAN_POINT('Ctrl Pts',(1.5,-3.39644906805545,6.00676874424307));
#46667=CARTESIAN_POINT('Ctrl Pts',(0.,-3.29194155025599,6.06467293808312));
#46668=CARTESIAN_POINT('Ctrl Pts',(1.5,-3.29194155025599,6.06467293808312));
#46669=CARTESIAN_POINT('Ctrl Pts',(0.,-3.18644717073138,6.12075905785849));
#46670=CARTESIAN_POINT('Ctrl Pts',(1.5,-3.18644717073138,6.12075905785849));
#46671=CARTESIAN_POINT('Ctrl Pts',(0.,-3.0799975547093,6.17501029000708));
#46672=CARTESIAN_POINT('Ctrl Pts',(1.5,-3.0799975547093,6.17501029000708));
#46673=CARTESIAN_POINT('Ctrl Pts',(0.,-2.97262461367203,6.22741037083384));
#46674=CARTESIAN_POINT('Ctrl Pts',(1.5,-2.97262461367203,6.22741037083384));
#46675=CARTESIAN_POINT('Ctrl Pts',(0.,-2.86436053589025,6.27794359158728));
#46676=CARTESIAN_POINT('Ctrl Pts',(1.5,-2.86436053589025,6.27794359158728));
#46677=CARTESIAN_POINT('Ctrl Pts',(0.,-2.75523777697418,6.32659480357071));
#46678=CARTESIAN_POINT('Ctrl Pts',(1.5,-2.75523777697418,6.32659480357071));
#46679=CARTESIAN_POINT('Ctrl Pts',(0.,-2.64528904995749,6.37334942227483));
#46680=CARTESIAN_POINT('Ctrl Pts',(1.5,-2.64528904995749,6.37334942227483));
#46681=CARTESIAN_POINT('Ctrl Pts',(0.,-2.53454731539729,6.41819343154555));
#46682=CARTESIAN_POINT('Ctrl Pts',(1.5,-2.53454731539729,6.41819343154555));
#46683=CARTESIAN_POINT('Ctrl Pts',(0.,-2.42304577148967,6.46111338778736));
#46684=CARTESIAN_POINT('Ctrl Pts',(1.5,-2.42304577148967,6.46111338778736));
#46685=CARTESIAN_POINT('Ctrl Pts',(0.,-2.31081784419995,6.50209642420256));
#46686=CARTESIAN_POINT('Ctrl Pts',(1.5,-2.31081784419995,6.50209642420256));
#46687=CARTESIAN_POINT('Ctrl Pts',(0.,-2.19789717740723,6.54113025506642));
#46688=CARTESIAN_POINT('Ctrl Pts',(1.5,-2.19789717740723,6.54113025506642));
#46689=CARTESIAN_POINT('Ctrl Pts',(0.,-2.08431762266816,6.57820317898663));
#46690=CARTESIAN_POINT('Ctrl Pts',(1.5,-2.08431762266816,6.57820317898663));
#46691=CARTESIAN_POINT('Ctrl Pts',(0.,-1.97011322899363,6.61330408219934));
#46692=CARTESIAN_POINT('Ctrl Pts',(1.5,-1.97011322899363,6.61330408219934));
#46693=CARTESIAN_POINT('Ctrl Pts',(0.,-1.85531823263787,6.6464224419019));
#46694=CARTESIAN_POINT('Ctrl Pts',(1.5,-1.85531823263787,6.6464224419019));
#46695=CARTESIAN_POINT('Ctrl Pts',(0.,-1.73996704689912,6.67754832962256));
#46696=CARTESIAN_POINT('Ctrl Pts',(1.5,-1.73996704689912,6.67754832962256));
#46697=CARTESIAN_POINT('Ctrl Pts',(0.,-1.62409425193149,6.70667241462728));
#46698=CARTESIAN_POINT('Ctrl Pts',(1.5,-1.62409425193149,6.70667241462728));
#46699=CARTESIAN_POINT('Ctrl Pts',(0.,-1.50773458426516,6.73378596628245));
#46700=CARTESIAN_POINT('Ctrl Pts',(1.5,-1.50773458426516,6.73378596628245));
#46701=CARTESIAN_POINT('Ctrl Pts',(0.,-1.39092292633645,6.75888085645522));
#46702=CARTESIAN_POINT('Ctrl Pts',(1.5,-1.39092292633645,6.75888085645522));
#46703=CARTESIAN_POINT('Ctrl Pts',(0.,-1.2736942960269,6.78194956195135));
#46704=CARTESIAN_POINT('Ctrl Pts',(1.5,-1.2736942960269,6.78194956195135));
#46705=CARTESIAN_POINT('Ctrl Pts',(0.,-1.156083836211,6.802985166991));
#46706=CARTESIAN_POINT('Ctrl Pts',(1.5,-1.156083836211,6.802985166991));
#46707=CARTESIAN_POINT('Ctrl Pts',(0.,-1.0381268043115,6.82198136572236));
#46708=CARTESIAN_POINT('Ctrl Pts',(1.5,-1.0381268043115,6.82198136572236));
#46709=CARTESIAN_POINT('Ctrl Pts',(0.,-0.919858561654649,6.83893246366822));
#46710=CARTESIAN_POINT('Ctrl Pts',(1.5,-0.919858561654649,6.83893246366822));
#46711=CARTESIAN_POINT('Ctrl Pts',(0.,-0.801314562831785,6.85383337921071));
#46712=CARTESIAN_POINT('Ctrl Pts',(1.5,-0.801314562831785,6.85383337921071));
#46713=CARTESIAN_POINT('Ctrl Pts',(0.,-0.682530345066844,6.86667964511437));
#46714=CARTESIAN_POINT('Ctrl Pts',(1.5,-0.682530345066844,6.86667964511437));
#46715=CARTESIAN_POINT('Ctrl Pts',(0.,-0.563541517588961,6.87746741008759));
#46716=CARTESIAN_POINT('Ctrl Pts',(1.5,-0.563541517588961,6.87746741008759));
#46717=CARTESIAN_POINT('Ctrl Pts',(0.,-0.444383751009606,6.88619344038256));
#46718=CARTESIAN_POINT('Ctrl Pts',(1.5,-0.444383751009606,6.88619344038256));
#46719=CARTESIAN_POINT('Ctrl Pts',(0.,-0.325092766592694,6.89285512031881));
#46720=CARTESIAN_POINT('Ctrl Pts',(1.5,-0.325092766592694,6.89285512031881));
#46721=CARTESIAN_POINT('Ctrl Pts',(0.,-0.205704325527824,6.89745045284557));
#46722=CARTESIAN_POINT('Ctrl Pts',(1.5,-0.205704325527824,6.89745045284557));
#46723=CARTESIAN_POINT('Ctrl Pts',(0.,-0.0862542182059904,6.89997806014265));
#46724=CARTESIAN_POINT('Ctrl Pts',(1.5,-0.0862542182059904,6.89997806014265));
#46725=CARTESIAN_POINT('Ctrl Pts',(0.,0.0332217465028425,6.90043718426019));
#46726=CARTESIAN_POINT('Ctrl Pts',(1.5,0.0332217465028425,6.90043718426019));
#46727=CARTESIAN_POINT('Ctrl Pts',(0.,0.152687751971073,6.89882768779694));
#46728=CARTESIAN_POINT('Ctrl Pts',(1.5,0.152687751971073,6.89882768779694));
#46729=CARTESIAN_POINT('Ctrl Pts',(0.,0.272107984548712,6.89515005348743));
#46730=CARTESIAN_POINT('Ctrl Pts',(1.5,0.272107984548712,6.89515005348743));
#46731=CARTESIAN_POINT('Ctrl Pts',(0.,0.39144664429895,6.88940538382782));
#46732=CARTESIAN_POINT('Ctrl Pts',(1.5,0.39144664429895,6.88940538382782));
#46733=CARTESIAN_POINT('Ctrl Pts',(0.,0.510667955734471,6.88159540074063));
#46734=CARTESIAN_POINT('Ctrl Pts',(1.5,0.510667955734471,6.88159540074063));
#46735=CARTESIAN_POINT('Ctrl Pts',(0.,0.629736178555366,6.871722445278));
#46736=CARTESIAN_POINT('Ctrl Pts',(1.5,0.629736178555366,6.871722445278));
#46737=CARTESIAN_POINT('Ctrl Pts',(0.,0.748615618389192,6.85978947736383));
#46738=CARTESIAN_POINT('Ctrl Pts',(1.5,0.748615618389192,6.85978947736383));
#46739=CARTESIAN_POINT('Ctrl Pts',(0.,0.867270637449732,6.84580007446996));
#46740=CARTESIAN_POINT('Ctrl Pts',(1.5,0.867270637449732,6.84580007446996));
#46741=CARTESIAN_POINT('Ctrl Pts',(0.,0.985665665199245,6.82975843033101));
#46742=CARTESIAN_POINT('Ctrl Pts',(1.5,0.985665665199245,6.82975843033101));
#46743=CARTESIAN_POINT('Ctrl Pts',(0.,1.10376520901494,6.81166935369773));
#46744=CARTESIAN_POINT('Ctrl Pts',(1.5,1.10376520901494,6.81166935369773));
#46745=CARTESIAN_POINT('Ctrl Pts',(0.,1.22153386486028,6.7915382671287));
#46746=CARTESIAN_POINT('Ctrl Pts',(1.5,1.22153386486028,6.7915382671287));
#46747=CARTESIAN_POINT('Ctrl Pts',(0.,1.33893632796192,6.76937120582047));
#46748=CARTESIAN_POINT('Ctrl Pts',(1.5,1.33893632796192,6.76937120582047));
#46749=CARTESIAN_POINT('Ctrl Pts',(0.,1.45593740331558,6.74517481533056));
#46750=CARTESIAN_POINT('Ctrl Pts',(1.5,1.45593740331558,6.74517481533056));
#46751=CARTESIAN_POINT('Ctrl Pts',(0.,1.57250201619893,6.71895634933867));
#46752=CARTESIAN_POINT('Ctrl Pts',(1.5,1.57250201619893,6.71895634933867));
#46753=CARTESIAN_POINT('Ctrl Pts',(0.,1.68859522269187,6.69072366744589));
#46754=CARTESIAN_POINT('Ctrl Pts',(1.5,1.68859522269187,6.69072366744589));
#46755=CARTESIAN_POINT('Ctrl Pts',(0.,1.80418222020506,6.66048523301177));
#46756=CARTESIAN_POINT('Ctrl Pts',(1.5,1.80418222020506,6.66048523301177));
#46757=CARTESIAN_POINT('Ctrl Pts',(0.,1.91922835801723,6.62825011102907));
#46758=CARTESIAN_POINT('Ctrl Pts',(1.5,1.91922835801723,6.62825011102907));
#46759=CARTESIAN_POINT('Ctrl Pts',(0.,2.03369914754119,6.59402796503178));
#46760=CARTESIAN_POINT('Ctrl Pts',(1.5,2.03369914754119,6.59402796503178));
#46761=CARTESIAN_POINT('Ctrl Pts',(0.,2.14756027260001,6.55782905404063));
#46762=CARTESIAN_POINT('Ctrl Pts',(1.5,2.14756027260001,6.55782905404063));
#46763=CARTESIAN_POINT('Ctrl Pts',(0.,2.26077759971389,6.51966422954576));
#46764=CARTESIAN_POINT('Ctrl Pts',(1.5,2.26077759971389,6.51966422954576));
#46765=CARTESIAN_POINT('Ctrl Pts',(0.,2.37331718839861,6.47954493252643));
#46766=CARTESIAN_POINT('Ctrl Pts',(1.5,2.37331718839861,6.47954493252643));
#46767=CARTESIAN_POINT('Ctrl Pts',(0.,2.48514530147589,6.4374831905076));
#46768=CARTESIAN_POINT('Ctrl Pts',(1.5,2.48514530147589,6.4374831905076));
#46769=CARTESIAN_POINT('Ctrl Pts',(0.,2.59622841504222,6.39349161339469));
#46770=CARTESIAN_POINT('Ctrl Pts',(1.5,2.59622841504222,6.39349161339469));
#46771=CARTESIAN_POINT('Ctrl Pts',(0.,2.70653322845103,6.34758338934495));
#46772=CARTESIAN_POINT('Ctrl Pts',(1.5,2.70653322845103,6.34758338934495));
#46773=CARTESIAN_POINT('Ctrl Pts',(0.,2.81602667430883,6.29977228067472));
#46774=CARTESIAN_POINT('Ctrl Pts',(1.5,2.81602667430883,6.29977228067472));
#46775=CARTESIAN_POINT('Ctrl Pts',(0.,2.92467592848589,6.25007261980284));
#46776=CARTESIAN_POINT('Ctrl Pts',(1.5,2.92467592848589,6.25007261980284));
#46777=CARTESIAN_POINT('Ctrl Pts',(0.,3.03244842014215,6.19849930522943));
#46778=CARTESIAN_POINT('Ctrl Pts',(1.5,3.03244842014215,6.19849930522943));
#46779=CARTESIAN_POINT('Ctrl Pts',(0.,3.13931184127864,6.14506779698229));
#46780=CARTESIAN_POINT('Ctrl Pts',(1.5,3.13931184127864,6.14506779698229));
#46781=CARTESIAN_POINT('Ctrl Pts',(0.,3.24523415630526,6.08979411209844));
#46782=CARTESIAN_POINT('Ctrl Pts',(1.5,3.24523415630526,6.08979411209844));
#46783=CARTESIAN_POINT('Ctrl Pts',(0.,3.35018361162562,6.03269482014039));
#46784=CARTESIAN_POINT('Ctrl Pts',(1.5,3.35018361162562,6.03269482014039));
#46785=CARTESIAN_POINT('Ctrl Pts',(0.,3.45412874523943,5.97378703874699));
#46786=CARTESIAN_POINT('Ctrl Pts',(1.5,3.45412874523943,5.97378703874699));
#46787=CARTESIAN_POINT('Ctrl Pts',(0.,3.55703839636324,5.91308842921844));
#46788=CARTESIAN_POINT('Ctrl Pts',(1.5,3.55703839636324,5.91308842921844));
#46789=CARTESIAN_POINT('Ctrl Pts',(0.,3.65888171459873,5.85061719009051));
#46790=CARTESIAN_POINT('Ctrl Pts',(1.5,3.65888171459873,5.85061719009051));
#46791=CARTESIAN_POINT('Ctrl Pts',(0.,3.75962816912046,5.78639205074214));
#46792=CARTESIAN_POINT('Ctrl Pts',(1.5,3.75962816912046,5.78639205074214));
#46793=CARTESIAN_POINT('Ctrl Pts',(0.,3.85924755788358,5.72043226503629));
#46794=CARTESIAN_POINT('Ctrl Pts',(1.5,3.85924755788358,5.72043226503629));
#46795=CARTESIAN_POINT('Ctrl Pts',(0.,3.95771001685206,5.65275760499367));
#46796=CARTESIAN_POINT('Ctrl Pts',(1.5,3.95771001685206,5.65275760499367));
#46797=CARTESIAN_POINT('Ctrl Pts',(0.,4.05498602924811,5.58338835449887));
#46798=CARTESIAN_POINT('Ctrl Pts',(1.5,4.05498602924811,5.58338835449887));
#46799=CARTESIAN_POINT('Ctrl Pts',(0.,4.15104643402264,5.51234530457567));
#46800=CARTESIAN_POINT('Ctrl Pts',(1.5,4.15104643402264,5.51234530457567));
#46801=CARTESIAN_POINT('Ctrl Pts',(0.,4.24586243434801,5.43964974869428));
#46802=CARTESIAN_POINT('Ctrl Pts',(1.5,4.24586243434801,5.43964974869428));
#46803=CARTESIAN_POINT('Ctrl Pts',(0.,4.33940560613354,5.36532347810979));
#46804=CARTESIAN_POINT('Ctrl Pts',(1.5,4.33940560613354,5.36532347810979));
#46805=CARTESIAN_POINT('Ctrl Pts',(0.,4.43164790656429,5.28938877723184));
#46806=CARTESIAN_POINT('Ctrl Pts',(1.5,4.43164790656429,5.28938877723184));
#46807=CARTESIAN_POINT('Ctrl Pts',(0.,4.52256168266372,5.2118684190248));
#46808=CARTESIAN_POINT('Ctrl Pts',(1.5,4.52256168266372,5.2118684190248));
#46809=CARTESIAN_POINT('Ctrl Pts',(0.,4.61211967957445,5.13278565383194));
#46810=CARTESIAN_POINT('Ctrl Pts',(1.5,4.61211967957445,5.13278565383194));
#46811=CARTESIAN_POINT('Ctrl Pts',(0.,4.70029504886408,5.05216419822939));
#46812=CARTESIAN_POINT('Ctrl Pts',(1.5,4.70029504886408,5.05216419822939));
#46813=CARTESIAN_POINT('Ctrl Pts',(0.,4.78706135685631,4.97002822390918));
#46814=CARTESIAN_POINT('Ctrl Pts',(1.5,4.78706135685631,4.97002822390918));
#46815=CARTESIAN_POINT('Ctrl Pts',(0.,4.87239259298801,4.88640234659105));
#46816=CARTESIAN_POINT('Ctrl Pts',(1.5,4.87239259298801,4.88640234659105));
#46817=CARTESIAN_POINT('Ctrl Pts',(0.,4.95626317819269,4.80131161496197));
#46818=CARTESIAN_POINT('Ctrl Pts',(1.5,4.95626317819269,4.80131161496197));
#46819=CARTESIAN_POINT('Ctrl Pts',(0.,5.03864797160205,4.71478151214967));
#46820=CARTESIAN_POINT('Ctrl Pts',(1.5,5.03864797160205,4.71478151214967));
#46821=CARTESIAN_POINT('Ctrl Pts',(0.,5.11952227727493,4.62683795722329));
#46822=CARTESIAN_POINT('Ctrl Pts',(1.5,5.11952227727493,4.62683795722329));
#46823=CARTESIAN_POINT('Ctrl Pts',(0.,5.19886185095397,4.53750730672122));
#46824=CARTESIAN_POINT('Ctrl Pts',(1.5,5.19886185095397,4.53750730672122));
#46825=CARTESIAN_POINT('Ctrl Pts',(0.,5.27664290685066,4.44681635620587));
#46826=CARTESIAN_POINT('Ctrl Pts',(1.5,5.27664290685066,4.44681635620587));
#46827=CARTESIAN_POINT('Ctrl Pts',(0.,5.35284212445892,4.35479234184536));
#46828=CARTESIAN_POINT('Ctrl Pts',(1.5,5.35284212445892,4.35479234184536));
#46829=CARTESIAN_POINT('Ctrl Pts',(0.,5.42743665671074,4.2614629103579));
#46830=CARTESIAN_POINT('Ctrl Pts',(1.5,5.42743665671074,4.2614629103579));
#46831=CARTESIAN_POINT('Ctrl Pts',(0.,5.50040413816131,4.16685608898156));
#46832=CARTESIAN_POINT('Ctrl Pts',(1.5,5.50040413816131,4.16685608898156));
#46833=CARTESIAN_POINT('Ctrl Pts',(0.,5.57172269320426,4.07100025546809));
#46834=CARTESIAN_POINT('Ctrl Pts',(1.5,5.57172269320426,4.07100025546809));
#46835=CARTESIAN_POINT('Ctrl Pts',(0.,5.64137094431753,3.97392410809942));
#46836=CARTESIAN_POINT('Ctrl Pts',(1.5,5.64137094431753,3.97392410809942));
#46837=CARTESIAN_POINT('Ctrl Pts',(0.,5.70932802034013,3.87565663572553));
#46838=CARTESIAN_POINT('Ctrl Pts',(1.5,5.70932802034013,3.87565663572553));
#46839=CARTESIAN_POINT('Ctrl Pts',(0.,5.77557355885907,3.7762271589849));
#46840=CARTESIAN_POINT('Ctrl Pts',(1.5,5.77557355885907,3.7762271589849));
#46841=CARTESIAN_POINT('Ctrl Pts',(0.,5.84008770862796,3.67566537154607));
#46842=CARTESIAN_POINT('Ctrl Pts',(1.5,5.84008770862796,3.67566537154607));
#46843=CARTESIAN_POINT('Ctrl Pts',(0.,5.90285113201758,3.57400138137221));
#46844=CARTESIAN_POINT('Ctrl Pts',(1.5,5.90285113201758,3.57400138137221));
#46845=CARTESIAN_POINT('Ctrl Pts',(0.,5.96384500749881,3.47126575200941));
#46846=CARTESIAN_POINT('Ctrl Pts',(1.5,5.96384500749881,3.47126575200941));
#46847=CARTESIAN_POINT('Ctrl Pts',(0.,6.0230510321579,3.36748954390066));
#46848=CARTESIAN_POINT('Ctrl Pts',(1.5,6.0230510321579,3.36748954390066));
#46849=CARTESIAN_POINT('Ctrl Pts',(0.,6.08045143492985,3.26270418832904));
#46850=CARTESIAN_POINT('Ctrl Pts',(1.5,6.08045143492985,3.26270418832904));
#46851=CARTESIAN_POINT('Ctrl Pts',(0.,6.1360289898651,3.15694136138284));
#46852=CARTESIAN_POINT('Ctrl Pts',(1.5,6.1360289898651,3.15694136138284));
#46853=CARTESIAN_POINT('Ctrl Pts',(0.,6.18976702943025,3.05023285793733));
#46854=CARTESIAN_POINT('Ctrl Pts',(1.5,6.18976702943025,3.05023285793733));
#46855=CARTESIAN_POINT('Ctrl Pts',(0.,6.24164945784326,2.94261046564829));
#46856=CARTESIAN_POINT('Ctrl Pts',(1.5,6.24164945784326,2.94261046564829));
#46857=CARTESIAN_POINT('Ctrl Pts',(0.,6.291660764444,2.83410583895225));
#46858=CARTESIAN_POINT('Ctrl Pts',(1.5,6.291660764444,2.83410583895225));
#46859=CARTESIAN_POINT('Ctrl Pts',(0.,6.339786009045,2.72475075998752));
#46860=CARTESIAN_POINT('Ctrl Pts',(1.5,6.339786009045,2.72475075998752));
#46861=CARTESIAN_POINT('Ctrl Pts',(0.,6.38601080731774,2.61457739952658));
#46862=CARTESIAN_POINT('Ctrl Pts',(1.5,6.38601080731774,2.61457739952658));
#46863=CARTESIAN_POINT('Ctrl Pts',(0.,6.43032131621382,2.50361857792934));
#46864=CARTESIAN_POINT('Ctrl Pts',(1.5,6.43032131621382,2.50361857792934));
#46865=CARTESIAN_POINT('Ctrl Pts',(0.,6.47270421942066,2.39190802612696));
#46866=CARTESIAN_POINT('Ctrl Pts',(1.5,6.47270421942066,2.39190802612696));
#46867=CARTESIAN_POINT('Ctrl Pts',(0.,6.51314671285136,2.27948064664619));
#46868=CARTESIAN_POINT('Ctrl Pts',(1.5,6.51314671285136,2.27948064664619));
#46869=CARTESIAN_POINT('Ctrl Pts',(0.,6.55163655192191,2.1663718749224));
#46870=CARTESIAN_POINT('Ctrl Pts',(1.5,6.55163655192191,2.1663718749224));
#46871=CARTESIAN_POINT('Ctrl Pts',(0.,6.58816209886384,2.05261704063847));
#46872=CARTESIAN_POINT('Ctrl Pts',(1.5,6.58816209886384,2.05261704063847));
#46873=CARTESIAN_POINT('Ctrl Pts',(0.,6.62271237007439,1.93825072906452));
#46874=CARTESIAN_POINT('Ctrl Pts',(1.5,6.62271237007439,1.93825072906452));
#46875=CARTESIAN_POINT('Ctrl Pts',(0.,6.65527708350579,1.82330614237472));
#46876=CARTESIAN_POINT('Ctrl Pts',(1.5,6.65527708350579,1.82330614237472));
#46877=CARTESIAN_POINT('Ctrl Pts',(0.,6.6858467060959,1.70781446091566));
#46878=CARTESIAN_POINT('Ctrl Pts',(1.5,6.6858467060959,1.70781446091566));
#46879=CARTESIAN_POINT('Ctrl Pts',(0.,6.71441235475264,1.59180628284183));
#46880=CARTESIAN_POINT('Ctrl Pts',(1.5,6.71441235475264,1.59180628284183));
#46881=CARTESIAN_POINT('Ctrl Pts',(0.,6.74096569737792,1.47531306373213));
#46882=CARTESIAN_POINT('Ctrl Pts',(1.5,6.74096569737792,1.47531306373213));
#46883=CARTESIAN_POINT('Ctrl Pts',(0.,6.76549885392711,1.35836855624325));
#46884=CARTESIAN_POINT('Ctrl Pts',(1.5,6.76549885392711,1.35836855624325));
#46885=CARTESIAN_POINT('Ctrl Pts',(0.,6.78800429750073,1.24101024985218));
#46886=CARTESIAN_POINT('Ctrl Pts',(1.5,6.78800429750073,1.24101024985218));
#46887=CARTESIAN_POINT('Ctrl Pts',(0.,6.80847475546411,1.12328081074528));
#46888=CARTESIAN_POINT('Ctrl Pts',(1.5,6.80847475546411,1.12328081074528));
#46889=CARTESIAN_POINT('Ctrl Pts',(0.,6.82690343687802,1.00522492629014));
#46890=CARTESIAN_POINT('Ctrl Pts',(1.5,6.82690343687802,1.00522492629014));
#46891=CARTESIAN_POINT('Ctrl Pts',(0.,6.84328425996227,0.886886149588873));
#46892=CARTESIAN_POINT('Ctrl Pts',(1.5,6.84328425996227,0.886886149588873));
#46893=CARTESIAN_POINT('Ctrl Pts',(0.,6.85761207960138,0.768303743989806));
#46894=CARTESIAN_POINT('Ctrl Pts',(1.5,6.85761207960138,0.768303743989806));
#46895=CARTESIAN_POINT('Ctrl Pts',(0.,6.8698829149006,0.649509527441057));
#46896=CARTESIAN_POINT('Ctrl Pts',(1.5,6.8698829149006,0.649509527441057));
#46897=CARTESIAN_POINT('Ctrl Pts',(0.,6.88009417680139,0.530524716562488));
#46898=CARTESIAN_POINT('Ctrl Pts',(1.5,6.88009417680139,0.530524716562488));
#46899=CARTESIAN_POINT('Ctrl Pts',(0.,6.88824437408576,0.411362046113686));
#46900=CARTESIAN_POINT('Ctrl Pts',(1.5,6.88824437408576,0.411362046113686));
#46901=CARTESIAN_POINT('Ctrl Pts',(0.,6.89311513036717,0.315894719735552));
#46902=CARTESIAN_POINT('Ctrl Pts',(1.5,6.89311513036717,0.315894719735552));
#46903=CARTESIAN_POINT('Ctrl Pts',(0.,6.89584032942016,0.244218013275557));
#46904=CARTESIAN_POINT('Ctrl Pts',(1.5,6.89584032942016,0.244218013275557));
#46905=CARTESIAN_POINT('Ctrl Pts',(0.,6.89724474811979,0.19639967087135));
#46906=CARTESIAN_POINT('Ctrl Pts',(1.5,6.89724474811979,0.19639967087135));
#46907=CARTESIAN_POINT('Ctrl Pts',(0.,6.89784386230235,0.172482031811515));
#46908=CARTESIAN_POINT('Ctrl Pts',(1.5,6.89784386230235,0.172482031811515));
#46909=CARTESIAN_POINT('',(0.15,6.89784386230235,0.172482031811515));
#46910=CARTESIAN_POINT('Ctrl Pts',(0.15,6.89784386230235,0.172482031811515));
#46911=CARTESIAN_POINT('Ctrl Pts',(0.15,6.89384976775196,0.33193295887695));
#46912=CARTESIAN_POINT('Ctrl Pts',(0.15,6.86721937301695,0.769068553785531));
#46913=CARTESIAN_POINT('Ctrl Pts',(0.15,6.55672403346259,2.80069104006913));
#46914=CARTESIAN_POINT('Ctrl Pts',(0.15,4.55753706787808,5.94536461879026));
#46915=CARTESIAN_POINT('Ctrl Pts',(0.15,0.47740476259414,7.22297137435857));
#46916=CARTESIAN_POINT('Ctrl Pts',(0.15,-1.94905218134993,6.66877212629907));
#46917=CARTESIAN_POINT('Ctrl Pts',(0.15,-3.08518241062154,6.18617418921297));
#46918=CARTESIAN_POINT('Ctrl Pts',(0.15,-3.64702096578107,5.88077380485089));
#46919=CARTESIAN_POINT('Ctrl Pts',(0.15,-5.26204057710086,4.712638335515));
#46920=CARTESIAN_POINT('Ctrl Pts',(0.15,-6.87917153567566,2.33560060230451));
#46921=CARTESIAN_POINT('Ctrl Pts',(0.15,-7.00981900784351,-0.786370144444264));
#46922=CARTESIAN_POINT('Ctrl Pts',(0.15,-6.18684609770483,-3.3390146085407));
#46923=CARTESIAN_POINT('Ctrl Pts',(0.15,-4.52929209771623,-5.56835397775588));
#46924=CARTESIAN_POINT('Ctrl Pts',(0.15,-1.64828395884492,-6.94189872669882));
#46925=CARTESIAN_POINT('Ctrl Pts',(0.15,1.31036395343999,-6.93807076453762));
#46926=CARTESIAN_POINT('Ctrl Pts',(0.15,3.04585995518473,-6.26002474355005));
#46927=CARTESIAN_POINT('Ctrl Pts',(0.15,3.89276415816284,-5.6989278508729));
#46928=CARTESIAN_POINT('Ctrl Pts',(0.15,4.50883595665535,-5.25964112637036));
#46929=CARTESIAN_POINT('Ctrl Pts',(0.15,5.52985079048928,-4.29339059730747));
#46930=CARTESIAN_POINT('Ctrl Pts',(0.15,6.22991610706792,-3.06655667805971));
#46931=CARTESIAN_POINT('Ctrl Pts',(0.15,6.74221885100022,-1.64238122846297));
#46932=CARTESIAN_POINT('Ctrl Pts',(0.15,6.87986895437252,-0.890015525613691));
#46933=CARTESIAN_POINT('Ctrl Pts',(0.15,6.89784369771306,-0.172488601988405));
#46934=CARTESIAN_POINT('',(0.,6.89784386230235,0.172482031811515));
#46935=CARTESIAN_POINT('Ctrl Pts',(0.15,6.89784402687909,-0.172475461633085));
#46936=CARTESIAN_POINT('Ctrl Pts',(0.15,6.87987054647832,-0.890006823484593));
#46937=CARTESIAN_POINT('Ctrl Pts',(0.15,6.74222033236675,-1.64237711033971));
#46938=CARTESIAN_POINT('Ctrl Pts',(0.15,6.22991610706792,-3.06655667805971));
#46939=CARTESIAN_POINT('Ctrl Pts',(0.15,5.52985079048928,-4.29339059730747));
#46940=CARTESIAN_POINT('Ctrl Pts',(0.15,4.50883595665535,-5.25964112637036));
#46941=CARTESIAN_POINT('Ctrl Pts',(0.15,3.89276415816284,-5.6989278508729));
#46942=CARTESIAN_POINT('Ctrl Pts',(0.15,3.04585995518473,-6.26002474355005));
#46943=CARTESIAN_POINT('Ctrl Pts',(0.15,1.31036395343999,-6.93807076453762));
#46944=CARTESIAN_POINT('Ctrl Pts',(0.15,-1.64828395884492,-6.94189872669882));
#46945=CARTESIAN_POINT('Ctrl Pts',(0.15,-4.52929209771623,-5.56835397775588));
#46946=CARTESIAN_POINT('Ctrl Pts',(0.15,-6.18684609770483,-3.3390146085407));
#46947=CARTESIAN_POINT('Ctrl Pts',(0.15,-7.00981900784351,-0.786370144444264));
#46948=CARTESIAN_POINT('Ctrl Pts',(0.15,-6.87917153567566,2.33560060230451));
#46949=CARTESIAN_POINT('Ctrl Pts',(0.15,-5.26204057710086,4.712638335515));
#46950=CARTESIAN_POINT('Ctrl Pts',(0.15,-3.64702096578107,5.88077380485089));
#46951=CARTESIAN_POINT('Ctrl Pts',(0.15,-3.08518241062154,6.18617418921297));
#46952=CARTESIAN_POINT('Ctrl Pts',(0.15,-1.94905218134993,6.66877212629907));
#46953=CARTESIAN_POINT('Ctrl Pts',(0.15,0.47740476259414,7.22297137435857));
#46954=CARTESIAN_POINT('Ctrl Pts',(0.15,4.55753706787808,5.94536461879026));
#46955=CARTESIAN_POINT('Ctrl Pts',(0.15,6.55672403346259,2.80069104006913));
#46956=CARTESIAN_POINT('Ctrl Pts',(0.15,6.86721937301695,0.769068553785531));
#46957=CARTESIAN_POINT('Ctrl Pts',(0.15,6.89384976775196,0.33193295887695));
#46958=CARTESIAN_POINT('Ctrl Pts',(0.15,6.89784386230235,0.172482031811515));
#46959=CARTESIAN_POINT('Ctrl Pts',(0.1,6.94782834788194,-0.173727521489497));
#46960=CARTESIAN_POINT('Ctrl Pts',(0.1,6.9297284773311,-0.89644913748462));
#46961=CARTESIAN_POINT('Ctrl Pts',(0.0999999999999999,6.79107540015654,
-1.65427761636173));
#46962=CARTESIAN_POINT('Ctrl Pts',(0.1,6.27506228900912,-3.08877763008951));
#46963=CARTESIAN_POINT('Ctrl Pts',(0.0999999999999999,5.56992168908083,
-4.32450087751743));
#46964=CARTESIAN_POINT('Ctrl Pts',(0.1,4.54150877965936,-5.29775537284816));
#46965=CARTESIAN_POINT('Ctrl Pts',(0.1,3.92097241788847,-5.74022297978704));
#46966=CARTESIAN_POINT('Ctrl Pts',(0.1,3.06793267773209,-6.30539378926051));
#46967=CARTESIAN_POINT('Ctrl Pts',(0.1,1.3198586472779,-6.98834205805805));
#46968=CARTESIAN_POINT('Ctrl Pts',(0.1,-1.66022698490003,-6.99220544238868));
#46969=CARTESIAN_POINT('Ctrl Pts',(0.1,-4.5621155749862,-5.60870389753307));
#46970=CARTESIAN_POINT('Ctrl Pts',(0.1,-6.23167543831412,-3.36320956230316));
#46971=CARTESIAN_POINT('Ctrl Pts',(0.1,-7.06061739245503,-0.792066536063253));
#46972=CARTESIAN_POINT('Ctrl Pts',(0.1,-6.92901318894491,2.35251318914951));
#46973=CARTESIAN_POINT('Ctrl Pts',(0.1,-5.30018968931025,4.74681443790138));
#46974=CARTESIAN_POINT('Ctrl Pts',(0.1,-3.67344113870542,5.92337668599479));
#46975=CARTESIAN_POINT('Ctrl Pts',(0.1,-3.10753747551775,6.23101823378308));
#46976=CARTESIAN_POINT('Ctrl Pts',(0.1,-1.96317749500257,6.71706621716312));
#46977=CARTESIAN_POINT('Ctrl Pts',(0.1,0.480873909248904,7.27533423073512));
#46978=CARTESIAN_POINT('Ctrl Pts',(0.0999999999999999,4.59054244474249,
5.98843108463992));
#46979=CARTESIAN_POINT('Ctrl Pts',(0.1,6.60427005889709,2.82099242255299));
#46980=CARTESIAN_POINT('Ctrl Pts',(0.1,6.91696548261244,0.77463982747282));
#46981=CARTESIAN_POINT('Ctrl Pts',(0.1,6.94381611987537,0.334338463222424));
#46982=CARTESIAN_POINT('Ctrl Pts',(0.1,6.94782818330531,0.17373409166339));
#46983=CARTESIAN_POINT('Ctrl Pts',(0.05,6.99781266888479,-0.174979581345908));
#46984=CARTESIAN_POINT('Ctrl Pts',(0.0499999999999999,6.9799655786341,-0.887320689053801));
#46985=CARTESIAN_POINT('Ctrl Pts',(0.0500000000000001,6.83996736785432,
-1.6648587174595));
#46986=CARTESIAN_POINT('Ctrl Pts',(0.0499999999999998,6.32027603624419,
-3.10810475947495));
#46987=CARTESIAN_POINT('Ctrl Pts',(0.0500000000000002,5.60999847637134,
-4.35544803176837));
#46988=CARTESIAN_POINT('Ctrl Pts',(0.0499999999999999,4.57419179627318,
-5.33545786922552));
#46989=CARTESIAN_POINT('Ctrl Pts',(0.05,3.9491897409667,-5.78118915940952));
#46990=CARTESIAN_POINT('Ctrl Pts',(0.05,3.09000963553784,-6.35042977939185));
#46991=CARTESIAN_POINT('Ctrl Pts',(0.05,1.32935705385206,-7.03856408743832));
#46992=CARTESIAN_POINT('Ctrl Pts',(0.0500000000000001,-1.6721716011548,
-7.0424409921364));
#46993=CARTESIAN_POINT('Ctrl Pts',(0.0499999999999999,-4.59493164670564,
-5.64906110396198));
#46994=CARTESIAN_POINT('Ctrl Pts',(0.05,-6.27651326142051,-3.38740106795732));
#46995=CARTESIAN_POINT('Ctrl Pts',(0.0499999999999999,-7.1114079969986,
-0.797768849285689));
#46996=CARTESIAN_POINT('Ctrl Pts',(0.05,-6.97887705298601,2.36946336996088));
#46997=CARTESIAN_POINT('Ctrl Pts',(0.0499999999999999,-5.33828367410731,
4.7809108444846));
#46998=CARTESIAN_POINT('Ctrl Pts',(0.05,-3.69988388432588,5.96601397199249));
#46999=CARTESIAN_POINT('Ctrl Pts',(0.05,-3.12989656095608,6.27581229321813));
#47000=CARTESIAN_POINT('Ctrl Pts',(0.05,-1.97729763925328,6.76545163088962));
#47001=CARTESIAN_POINT('Ctrl Pts',(0.05,0.484314506462699,7.3276264869806));
#47002=CARTESIAN_POINT('Ctrl Pts',(0.05,4.62360674015065,6.03155341936274));
#47003=CARTESIAN_POINT('Ctrl Pts',(0.05,6.65171580610762,2.84126752862509));
#47004=CARTESIAN_POINT('Ctrl Pts',(0.05,6.96676043939284,0.780220974861774));
#47005=CARTESIAN_POINT('Ctrl Pts',(0.05,6.99374990469226,0.336735818443863));
#47006=CARTESIAN_POINT('Ctrl Pts',(0.05,6.99781250430828,0.174986151515265));
#47007=CARTESIAN_POINT('Ctrl Pts',(0.,7.04779698988764,-0.176231641202319));
#47008=CARTESIAN_POINT('Ctrl Pts',(0.,7.02982350948688,-0.893763003053827));
#47009=CARTESIAN_POINT('Ctrl Pts',(0.,6.88882243564412,-1.67675922348152));
#47010=CARTESIAN_POINT('Ctrl Pts',(0.,6.3654222181854,-3.13032571150475));
#47011=CARTESIAN_POINT('Ctrl Pts',(0.,5.6500693749629,-4.38655831197832));
#47012=CARTESIAN_POINT('Ctrl Pts',(0.,4.60686461927718,-5.37357211570332));
#47013=CARTESIAN_POINT('Ctrl Pts',(0.,3.97739800069233,-5.82248428832366));
#47014=CARTESIAN_POINT('Ctrl Pts',(0.,3.11208235808519,-6.39579882510231));
#47015=CARTESIAN_POINT('Ctrl Pts',(0.,1.33885174768997,-7.08883538095876));
#47016=CARTESIAN_POINT('Ctrl Pts',(0.,-1.68411462720991,-7.09274770782626));
#47017=CARTESIAN_POINT('Ctrl Pts',(0.,-4.6277551239756,-5.68941102373917));
#47018=CARTESIAN_POINT('Ctrl Pts',(0.,-6.32134260202981,-3.41159602171978));
#47019=CARTESIAN_POINT('Ctrl Pts',(0.,-7.16220638161012,-0.803465240904679));
#47020=CARTESIAN_POINT('Ctrl Pts',(0.,-7.02871870625526,2.38637595680587));
#47021=CARTESIAN_POINT('Ctrl Pts',(0.,-5.37643278631671,4.81508694687098));
#47022=CARTESIAN_POINT('Ctrl Pts',(0.,-3.72630405725022,6.00861685313639));
#47023=CARTESIAN_POINT('Ctrl Pts',(0.,-3.15225162585228,6.32065633778824));
#47024=CARTESIAN_POINT('Ctrl Pts',(0.,-1.99142295290593,6.81374572175368));
#47025=CARTESIAN_POINT('Ctrl Pts',(0.,0.487783653117462,7.37998934335715));
#47026=CARTESIAN_POINT('Ctrl Pts',(0.,4.65661211701506,6.07461988521239));
#47027=CARTESIAN_POINT('Ctrl Pts',(0.,6.69926183154212,2.86156891110894));
#47028=CARTESIAN_POINT('Ctrl Pts',(0.,7.01650654898832,0.785792248549063));
#47029=CARTESIAN_POINT('Ctrl Pts',(0.,7.04371625681567,0.339141322789337));
#47030=CARTESIAN_POINT('Ctrl Pts',(0.,7.04779682531124,0.17623821136714));
#47031=CARTESIAN_POINT('',(0.,7.0477969074555,0.176234926281131));
#47032=CARTESIAN_POINT('Ctrl Pts',(0.,7.04779682531124,0.17623821136714));
#47033=CARTESIAN_POINT('Ctrl Pts',(0.05,6.99781250430828,0.174986151515265));
#47034=CARTESIAN_POINT('Ctrl Pts',(0.1,6.94782818330531,0.17373409166339));
#47035=CARTESIAN_POINT('Ctrl Pts',(0.15,6.89784386230235,0.172482031811515));
#47036=CARTESIAN_POINT('Ctrl Pts',(0.,7.04779698988764,-0.176231641202319));
#47037=CARTESIAN_POINT('Ctrl Pts',(0.,7.02982350948688,-0.893763003053827));
#47038=CARTESIAN_POINT('Ctrl Pts',(0.,6.88882243564412,-1.67675922348152));
#47039=CARTESIAN_POINT('Ctrl Pts',(0.,6.3654222181854,-3.13032571150475));
#47040=CARTESIAN_POINT('Ctrl Pts',(0.,5.6500693749629,-4.38655831197832));
#47041=CARTESIAN_POINT('Ctrl Pts',(0.,4.60686461927718,-5.37357211570332));
#47042=CARTESIAN_POINT('Ctrl Pts',(0.,3.97739800069233,-5.82248428832366));
#47043=CARTESIAN_POINT('Ctrl Pts',(0.,3.11208235808519,-6.39579882510231));
#47044=CARTESIAN_POINT('Ctrl Pts',(0.,1.33885174768997,-7.08883538095876));
#47045=CARTESIAN_POINT('Ctrl Pts',(0.,-1.68411462720991,-7.09274770782626));
#47046=CARTESIAN_POINT('Ctrl Pts',(0.,-4.6277551239756,-5.68941102373917));
#47047=CARTESIAN_POINT('Ctrl Pts',(0.,-6.32134260202981,-3.41159602171978));
#47048=CARTESIAN_POINT('Ctrl Pts',(0.,-7.16220638161012,-0.803465240904679));
#47049=CARTESIAN_POINT('Ctrl Pts',(0.,-7.02871870625526,2.38637595680587));
#47050=CARTESIAN_POINT('Ctrl Pts',(0.,-5.37643278631671,4.81508694687098));
#47051=CARTESIAN_POINT('Ctrl Pts',(0.,-3.72630405725022,6.00861685313639));
#47052=CARTESIAN_POINT('Ctrl Pts',(0.,-3.15225162585228,6.32065633778824));
#47053=CARTESIAN_POINT('Ctrl Pts',(0.,-1.99142295290593,6.81374572175368));
#47054=CARTESIAN_POINT('Ctrl Pts',(0.,0.487783653117462,7.37998934335715));
#47055=CARTESIAN_POINT('Ctrl Pts',(0.,4.65661211701506,6.07461988521239));
#47056=CARTESIAN_POINT('Ctrl Pts',(0.,6.69926183154212,2.86156891110894));
#47057=CARTESIAN_POINT('Ctrl Pts',(0.,7.01650654898832,0.785792248549063));
#47058=CARTESIAN_POINT('Ctrl Pts',(0.,7.04371625681567,0.339141322789337));
#47059=CARTESIAN_POINT('Ctrl Pts',(0.,7.04779682531124,0.17623821136714));
#47060=CARTESIAN_POINT('Origin',(0.,6.89784386230235,0.172482031811515));
#47061=CARTESIAN_POINT('',(1.5,6.89784386230235,0.172482031811515));
#47062=CARTESIAN_POINT('',(0.,6.89784386230235,0.172482031811515));
#47063=CARTESIAN_POINT('Origin',(1.5,-0.0015497354906735,4.21884749357559E-14));
#47064=CARTESIAN_POINT('Origin',(0.,-0.0015497354906735,4.21884749357559E-14));
#60348=UNCERTAINTY_MEASURE_WITH_UNIT(LENGTH_MEASURE(0.01),#60366,
'DISTANCE_ACCURACY_VALUE',
'Maximum model space distance between geometric entities at asserted c
onnectivities');
#60353=UNCERTAINTY_MEASURE_WITH_UNIT(LENGTH_MEASURE(0.01),#60366,
'DISTANCE_ACCURACY_VALUE',
'Maximum model space distance between geometric entities at asserted c
onnectivities');
#60360=(
GEOMETRIC_REPRESENTATION_CONTEXT(3)
GLOBAL_UNCERTAINTY_ASSIGNED_CONTEXT((#60348))
GLOBAL_UNIT_ASSIGNED_CONTEXT((#60366,#60368,#60369))
REPRESENTATION_CONTEXT('','3D')
);
#60365=(
GEOMETRIC_REPRESENTATION_CONTEXT(3)
GLOBAL_UNCERTAINTY_ASSIGNED_CONTEXT((#60353))
GLOBAL_UNIT_ASSIGNED_CONTEXT((#60366,#60368,#60369))
REPRESENTATION_CONTEXT('','3D')
);
#60366=(
LENGTH_UNIT()
NAMED_UNIT(*)
SI_UNIT(.MILLI.,.METRE.)
);
#60368=(
NAMED_UNIT(*)
PLANE_ANGLE_UNIT()
SI_UNIT($,.RADIAN.)
);
#60369=(
NAMED_UNIT(*)
SI_UNIT($,.STERADIAN.)
SOLID_ANGLE_UNIT()
);
#60376=SHAPE_DEFINITION_REPRESENTATION(#60387,#60412);
#60387=PRODUCT_DEFINITION_SHAPE('',$,#60424);
#60412=SHAPE_REPRESENTATION('',(#19226),#60360);
#60417=PRODUCT_DEFINITION_CONTEXT('part definition',#60452,'design');
#60424=PRODUCT_DEFINITION('2026-10-25-00-06-35-685',
'08_Piston_Ring_Compressor_D16',#60435,#60417);
#60435=PRODUCT_DEFINITION_FORMATION('',$,#60460);
#60452=APPLICATION_CONTEXT(
'Core Data for Automotive Mechanical Design Process');
#60453=PRODUCT_CONTEXT('part definition',#60452,'mechanical');
#60460=PRODUCT('2026-10-25-00-06-35-685',
'08_Piston_Ring_Compressor_D16',$,(#60453));
#60507=COLOUR_RGB('Light Blue',0.38,0.62,0.78);
#60508=FILL_AREA_STYLE_COLOUR('',#60507);
#60509=FILL_AREA_STYLE('',(#60508));
#60510=SURFACE_STYLE_FILL_AREA(#60509);
#60511=SURFACE_SIDE_STYLE('',(#60510));
#60512=SURFACE_STYLE_USAGE(.BOTH.,#60511);
#60513=PRESENTATION_STYLE_ASSIGNMENT((#60512));
ENDSEC;
END-ISO-10303-21;
